ISO-10303-21;
HEADER;
/* Generated by software containing ST-Developer
 * from STEP Tools, Inc. (www.steptools.com) 
 */

FILE_DESCRIPTION(
/* description */ (''),
/* implementation_level */ '2;1');

FILE_NAME(
/* name */ '12_Taper_Roller_Bearing_30205_Cone_Assembly.step',
/* time_stamp */ '2026-10-23T00:52:27+05:00',
/* author */ (''),
/* organization */ (''),
/* preprocessor_version */ 'ST-DEVELOPER v20.2',
/* originating_system */ 'Autodesk Translation Framework v15.15.0.0',
/* authorisation */ '');

FILE_SCHEMA (('AUTOMOTIVE_DESIGN { 1 0 10303 214 3 1 1 }'));
ENDSEC;

DATA;
#10=MECHANICAL_DESIGN_GEOMETRIC_PRESENTATION_REPRESENTATION('',(#1570),#59204);
#191=ELLIPSE('',#24235,2.14723853173756,2.09817147851385);
#192=ELLIPSE('',#24236,1.89123203768515,1.8480150491299);
#193=ELLIPSE('',#24237,2.14723853173756,2.09817147851385);
#194=ELLIPSE('',#24238,1.89123203768515,1.8480150491299);
#195=ELLIPSE('',#24239,2.14723853173756,2.09817147851385);
#196=ELLIPSE('',#24240,1.89123203768515,1.8480150491299);
#197=ELLIPSE('',#24241,2.14723853173756,2.09817147851385);
#198=ELLIPSE('',#24242,1.89123203768515,1.8480150491299);
#199=ELLIPSE('',#24243,2.14723853173756,2.09817147851385);
#200=ELLIPSE('',#24244,1.89123203768515,1.8480150491299);
#201=ELLIPSE('',#24245,2.14723853173756,2.09817147851385);
#202=ELLIPSE('',#24246,1.89123203768515,1.8480150491299);
#203=ELLIPSE('',#24247,2.14723853173756,2.09817147851385);
#204=ELLIPSE('',#24248,1.89123203768515,1.8480150491299);
#205=ELLIPSE('',#24249,2.14723853173756,2.09817147851384);
#206=ELLIPSE('',#24250,1.89123203768515,1.8480150491299);
#207=ELLIPSE('',#24251,2.14723853173756,2.09817147851385);
#208=ELLIPSE('',#24252,1.89123203768515,1.8480150491299);
#209=ELLIPSE('',#24253,2.14723853173756,2.09817147851385);
#210=ELLIPSE('',#24254,1.89123203768515,1.8480150491299);
#211=ELLIPSE('',#24255,2.14723853173756,2.09817147851385);
#212=ELLIPSE('',#24256,1.89123203768515,1.8480150491299);
#213=ELLIPSE('',#24257,2.14723853173756,2.09817147851385);
#214=ELLIPSE('',#24258,1.89123203768515,1.8480150491299);
#215=ELLIPSE('',#24259,2.14723853173756,2.09817147851384);
#216=ELLIPSE('',#24260,1.89123203768515,1.8480150491299);
#217=ELLIPSE('',#24261,2.14723853173756,2.09817147851384);
#218=ELLIPSE('',#24262,1.89123203768515,1.8480150491299);
#219=ELLIPSE('',#24263,2.14723853173756,2.09817147851385);
#220=ELLIPSE('',#24264,1.89123203768515,1.8480150491299);
#221=ELLIPSE('',#24265,2.14723853173756,2.09817147851385);
#222=ELLIPSE('',#24266,1.89123203768515,1.8480150491299);
#223=ELLIPSE('',#24267,1.89123203768515,1.8480150491299);
#224=ELLIPSE('',#24268,2.14723853173756,2.09817147851385);
#225=ELLIPSE('',#24272,2.2310239828778,2.18004232858406);
#226=ELLIPSE('',#24273,1.97501748882539,1.92988589920012);
#227=ELLIPSE('',#24274,2.2310239828778,2.18004232858406);
#228=ELLIPSE('',#24275,1.97501748882539,1.92988589920012);
#229=ELLIPSE('',#24276,2.2310239828778,2.18004232858406);
#230=ELLIPSE('',#24277,1.97501748882539,1.92988589920012);
#231=ELLIPSE('',#24278,2.2310239828778,2.18004232858406);
#232=ELLIPSE('',#24279,1.97501748882539,1.92988589920012);
#233=ELLIPSE('',#24280,2.2310239828778,2.18004232858406);
#234=ELLIPSE('',#24281,1.97501748882539,1.92988589920012);
#235=ELLIPSE('',#24282,2.2310239828778,2.18004232858406);
#236=ELLIPSE('',#24283,1.9750174888254,1.92988589920012);
#237=ELLIPSE('',#24284,2.2310239828778,2.18004232858406);
#238=ELLIPSE('',#24285,1.97501748882539,1.92988589920012);
#239=ELLIPSE('',#24286,2.2310239828778,2.18004232858406);
#240=ELLIPSE('',#24287,1.97501748882539,1.92988589920012);
#241=ELLIPSE('',#24288,2.2310239828778,2.18004232858406);
#242=ELLIPSE('',#24289,1.97501748882539,1.92988589920012);
#243=ELLIPSE('',#24290,2.2310239828778,2.18004232858406);
#244=ELLIPSE('',#24291,1.97501748882539,1.92988589920012);
#245=ELLIPSE('',#24292,2.2310239828778,2.18004232858406);
#246=ELLIPSE('',#24293,1.97501748882539,1.92988589920012);
#247=ELLIPSE('',#24294,2.2310239828778,2.18004232858406);
#248=ELLIPSE('',#24295,1.97501748882539,1.92988589920012);
#249=ELLIPSE('',#24296,2.2310239828778,2.18004232858406);
#250=ELLIPSE('',#24297,1.97501748882539,1.92988589920012);
#251=ELLIPSE('',#24298,2.2310239828778,2.18004232858406);
#252=ELLIPSE('',#24299,1.97501748882539,1.92988589920012);
#253=ELLIPSE('',#24300,2.2310239828778,2.18004232858406);
#254=ELLIPSE('',#24301,1.97501748882539,1.92988589920012);
#255=ELLIPSE('',#24302,2.2310239828778,2.18004232858406);
#256=ELLIPSE('',#24303,1.97501748882539,1.92988589920012);
#257=ELLIPSE('',#24304,2.2310239828778,2.18004232858406);
#258=ELLIPSE('',#24305,1.97501748882539,1.92988589920012);
#259=ELLIPSE('',#24312,1.60810685188985,1.57186069047033);
#260=ELLIPSE('',#24318,0.349707645748017,0.3420563457837);
#261=ELLIPSE('',#24324,1.60810685188985,1.57186069047032);
#262=ELLIPSE('',#24330,0.349707645748017,0.3420563457837);
#263=ELLIPSE('',#24336,1.60810685188985,1.57186069047033);
#264=ELLIPSE('',#24342,0.349707645748017,0.3420563457837);
#265=ELLIPSE('',#24348,1.60810685188985,1.57186069047033);
#266=ELLIPSE('',#24354,0.349707645748017,0.3420563457837);
#267=ELLIPSE('',#24360,1.60810685188985,1.57186069047032);
#268=ELLIPSE('',#24366,0.349707645748018,0.3420563457837);
#269=ELLIPSE('',#24372,1.60810685188985,1.57186069047033);
#270=ELLIPSE('',#24378,0.349707645748017,0.3420563457837);
#271=ELLIPSE('',#24384,1.60810685188985,1.57186069047033);
#272=ELLIPSE('',#24390,0.349707645748017,0.3420563457837);
#273=ELLIPSE('',#24396,1.60810685188985,1.57186069047033);
#274=ELLIPSE('',#24402,0.349707645748017,0.3420563457837);
#275=ELLIPSE('',#24408,1.60810685188985,1.57186069047032);
#276=ELLIPSE('',#24414,0.349707645748017,0.3420563457837);
#277=ELLIPSE('',#24420,1.60810685188985,1.57186069047033);
#278=ELLIPSE('',#24426,0.349707645748018,0.3420563457837);
#279=ELLIPSE('',#24432,1.60810685188985,1.57186069047033);
#280=ELLIPSE('',#24438,0.349707645748017,0.3420563457837);
#281=ELLIPSE('',#24444,1.60810685188985,1.57186069047033);
#282=ELLIPSE('',#24450,0.349707645748017,0.3420563457837);
#283=ELLIPSE('',#24456,1.60810685188985,1.57186069047032);
#284=ELLIPSE('',#24462,0.349707645748017,0.3420563457837);
#285=ELLIPSE('',#24468,1.60810685188985,1.57186069047032);
#286=ELLIPSE('',#24474,0.349707645748017,0.3420563457837);
#287=ELLIPSE('',#24480,1.60810685188985,1.57186069047032);
#288=ELLIPSE('',#24486,0.349707645748017,0.3420563457837);
#289=ELLIPSE('',#24492,1.60810685188985,1.57186069047033);
#290=ELLIPSE('',#24498,0.349707645748017,0.3420563457837);
#291=ELLIPSE('',#24506,1.60810685188985,1.57186069047033);
#292=ELLIPSE('',#24511,0.349707645748017,0.3420563457837);
#293=ELLIPSE('',#24515,0.349707645748017,0.3420563457837);
#294=ELLIPSE('',#24539,0.349707645748017,0.3420563457837);
#295=ELLIPSE('',#24543,0.349707645748017,0.3420563457837);
#296=ELLIPSE('',#24547,0.349707645748017,0.3420563457837);
#297=ELLIPSE('',#24551,0.349707645748018,0.3420563457837);
#298=ELLIPSE('',#24555,0.349707645748017,0.3420563457837);
#299=ELLIPSE('',#24559,0.349707645748017,0.3420563457837);
#300=ELLIPSE('',#24563,0.349707645748017,0.3420563457837);
#301=ELLIPSE('',#24567,0.349707645748017,0.3420563457837);
#302=ELLIPSE('',#24571,0.349707645748018,0.3420563457837);
#303=ELLIPSE('',#24575,0.349707645748017,0.3420563457837);
#304=ELLIPSE('',#24579,0.349707645748017,0.3420563457837);
#305=ELLIPSE('',#24583,0.349707645748017,0.3420563457837);
#306=ELLIPSE('',#24587,0.349707645748017,0.3420563457837);
#307=ELLIPSE('',#24591,0.349707645748017,0.3420563457837);
#308=ELLIPSE('',#24595,0.349707645748017,0.3420563457837);
#309=ELLIPSE('',#24597,0.349707645748017,0.3420563457837);
#1175=B_SPLINE_CURVE_WITH_KNOTS('',3,(#47413,#47414,#47415,#47416),
 .UNSPECIFIED.,.F.,.F.,(4,4),(1.05088688293601,2.10047487645352),
 .UNSPECIFIED.);
#1176=B_SPLINE_CURVE_WITH_KNOTS('',3,(#47419,#47420,#47421,#47422),
 .UNSPECIFIED.,.F.,.F.,(4,4),(1.06882494380393,2.11841293732144),
 .UNSPECIFIED.);
#1177=B_SPLINE_CURVE_WITH_KNOTS('',3,(#47427,#47428,#47429,#47430),
 .UNSPECIFIED.,.F.,.F.,(4,4),(1.098090767842,2.14756146588325),
 .UNSPECIFIED.);
#1178=B_SPLINE_CURVE_WITH_KNOTS('',3,(#47433,#47434,#47435,#47436),
 .UNSPECIFIED.,.F.,.F.,(4,4),(1.07645732586084,2.12592802390209),
 .UNSPECIFIED.);
#1179=B_SPLINE_CURVE_WITH_KNOTS('',3,(#47441,#47442,#47443,#47444),
 .UNSPECIFIED.,.F.,.F.,(4,4),(1.06876863774445,2.11830775146031),
 .UNSPECIFIED.);
#1180=B_SPLINE_CURVE_WITH_KNOTS('',3,(#47447,#47448,#47449,#47450),
 .UNSPECIFIED.,.F.,.F.,(4,4),(1.07183362023116,2.12137273394702),
 .UNSPECIFIED.);
#1181=B_SPLINE_CURVE_WITH_KNOTS('',3,(#47455,#47456,#47457,#47458),
 .UNSPECIFIED.,.F.,.F.,(4,4),(1.00966173528769,2.0593901610072),
 .UNSPECIFIED.);
#1182=B_SPLINE_CURVE_WITH_KNOTS('',3,(#47461,#47462,#47463,#47464),
 .UNSPECIFIED.,.F.,.F.,(4,4),(1.05659594524126,2.10632437096077),
 .UNSPECIFIED.);
#1183=B_SPLINE_CURVE_WITH_KNOTS('',3,(#47469,#47470,#47471,#47472),
 .UNSPECIFIED.,.F.,.F.,(4,4),(1.03463183846597,2.08427034714712),
 .UNSPECIFIED.);
#1184=B_SPLINE_CURVE_WITH_KNOTS('',3,(#47475,#47476,#47477,#47478),
 .UNSPECIFIED.,.F.,.F.,(4,4),(1.06519471367074,2.1148332223519),
 .UNSPECIFIED.);
#1185=B_SPLINE_CURVE_WITH_KNOTS('',3,(#47483,#47484,#47485,#47486),
 .UNSPECIFIED.,.F.,.F.,(4,4),(1.09726472627115,2.14673867240921),
 .UNSPECIFIED.);
#1186=B_SPLINE_CURVE_WITH_KNOTS('',3,(#47489,#47490,#47491,#47492),
 .UNSPECIFIED.,.F.,.F.,(4,4),(1.07572637127808,2.12520031741614),
 .UNSPECIFIED.);
#1187=B_SPLINE_CURVE_WITH_KNOTS('',3,(#47497,#47498,#47499,#47500),
 .UNSPECIFIED.,.F.,.F.,(4,4),(1.08743350871975,2.13692892862863),
 .UNSPECIFIED.);
#1188=B_SPLINE_CURVE_WITH_KNOTS('',3,(#47503,#47504,#47505,#47506),
 .UNSPECIFIED.,.F.,.F.,(4,4),(1.07417908634448,2.12367450625336),
 .UNSPECIFIED.);
#1189=B_SPLINE_CURVE_WITH_KNOTS('',3,(#47511,#47512,#47513,#47514),
 .UNSPECIFIED.,.F.,.F.,(4,4),(1.02070861103776,2.07039533198825),
 .UNSPECIFIED.);
#1190=B_SPLINE_CURVE_WITH_KNOTS('',3,(#47517,#47518,#47519,#47520),
 .UNSPECIFIED.,.F.,.F.,(4,4),(1.06098917218957,2.11067589314006),
 .UNSPECIFIED.);
#1191=B_SPLINE_CURVE_WITH_KNOTS('',3,(#47525,#47526,#47527,#47528),
 .UNSPECIFIED.,.F.,.F.,(4,4),(1.02070861103776,2.07039533198825),
 .UNSPECIFIED.);
#1192=B_SPLINE_CURVE_WITH_KNOTS('',3,(#47531,#47532,#47533,#47534),
 .UNSPECIFIED.,.F.,.F.,(4,4),(1.06098917218957,2.11067589314006),
 .UNSPECIFIED.);
#1193=B_SPLINE_CURVE_WITH_KNOTS('',3,(#47539,#47540,#47541,#47542),
 .UNSPECIFIED.,.F.,.F.,(4,4),(1.08743350871974,2.13692892862862),
 .UNSPECIFIED.);
#1194=B_SPLINE_CURVE_WITH_KNOTS('',3,(#47545,#47546,#47547,#47548),
 .UNSPECIFIED.,.F.,.F.,(4,4),(1.07417908634448,2.12367450625336),
 .UNSPECIFIED.);
#1195=B_SPLINE_CURVE_WITH_KNOTS('',3,(#47553,#47554,#47555,#47556),
 .UNSPECIFIED.,.F.,.F.,(4,4),(1.09726472627116,2.14673867240921),
 .UNSPECIFIED.);
#1196=B_SPLINE_CURVE_WITH_KNOTS('',3,(#47559,#47560,#47561,#47562),
 .UNSPECIFIED.,.F.,.F.,(4,4),(1.07572637127808,2.12520031741614),
 .UNSPECIFIED.);
#1197=B_SPLINE_CURVE_WITH_KNOTS('',3,(#47567,#47568,#47569,#47570),
 .UNSPECIFIED.,.F.,.F.,(4,4),(1.03463183846599,2.08427034714714),
 .UNSPECIFIED.);
#1198=B_SPLINE_CURVE_WITH_KNOTS('',3,(#47573,#47574,#47575,#47576),
 .UNSPECIFIED.,.F.,.F.,(4,4),(1.06519471367074,2.1148332223519),
 .UNSPECIFIED.);
#1199=B_SPLINE_CURVE_WITH_KNOTS('',3,(#47581,#47582,#47583,#47584),
 .UNSPECIFIED.,.F.,.F.,(4,4),(1.00966173528769,2.0593901610072),
 .UNSPECIFIED.);
#1200=B_SPLINE_CURVE_WITH_KNOTS('',3,(#47587,#47588,#47589,#47590),
 .UNSPECIFIED.,.F.,.F.,(4,4),(1.05659594524126,2.10632437096077),
 .UNSPECIFIED.);
#1201=B_SPLINE_CURVE_WITH_KNOTS('',3,(#47595,#47596,#47597,#47598),
 .UNSPECIFIED.,.F.,.F.,(4,4),(1.06876863774445,2.11830775146031),
 .UNSPECIFIED.);
#1202=B_SPLINE_CURVE_WITH_KNOTS('',3,(#47601,#47602,#47603,#47604),
 .UNSPECIFIED.,.F.,.F.,(4,4),(1.07183362023116,2.12137273394701),
 .UNSPECIFIED.);
#1203=B_SPLINE_CURVE_WITH_KNOTS('',3,(#47609,#47610,#47611,#47612),
 .UNSPECIFIED.,.F.,.F.,(4,4),(1.09809076783139,2.14756146587266),
 .UNSPECIFIED.);
#1204=B_SPLINE_CURVE_WITH_KNOTS('',3,(#47615,#47616,#47617,#47618),
 .UNSPECIFIED.,.F.,.F.,(4,4),(1.07645732586072,2.12592802390199),
 .UNSPECIFIED.);
#1205=B_SPLINE_CURVE_WITH_KNOTS('',3,(#47623,#47624,#47625,#47626),
 .UNSPECIFIED.,.F.,.F.,(4,4),(1.05088688291748,2.10047487643504),
 .UNSPECIFIED.);
#1206=B_SPLINE_CURVE_WITH_KNOTS('',3,(#47629,#47630,#47631,#47632),
 .UNSPECIFIED.,.F.,.F.,(4,4),(1.06882494380372,2.11841293732128),
 .UNSPECIFIED.);
#1207=B_SPLINE_CURVE_WITH_KNOTS('',3,(#47635,#47636,#47637,#47638),
 .UNSPECIFIED.,.F.,.F.,(4,4),(1.00183351673943,2.05159618842433),
 .UNSPECIFIED.);
#1208=B_SPLINE_CURVE_WITH_KNOTS('',3,(#47642,#47643,#47644,#47645),
 .UNSPECIFIED.,.F.,.F.,(4,4),(1.05075063815515,2.10051330984005),
 .UNSPECIFIED.);
#1209=B_SPLINE_CURVE_WITH_KNOTS('',3,(#47657,#47658,#47659,#47660),
 .UNSPECIFIED.,.F.,.F.,(4,4),(1.0651631905772,2.1146873922484),
 .UNSPECIFIED.);
#1210=B_SPLINE_CURVE_WITH_KNOTS('',3,(#47663,#47664,#47665,#47666),
 .UNSPECIFIED.,.F.,.F.,(4,4),(1.08410770108472,2.13363190275592),
 .UNSPECIFIED.);
#1211=B_SPLINE_CURVE_WITH_KNOTS('',3,(#47671,#47672,#47673,#47674),
 .UNSPECIFIED.,.F.,.F.,(4,4),(1.09826811480986,2.14770347966715),
 .UNSPECIFIED.);
#1212=B_SPLINE_CURVE_WITH_KNOTS('',3,(#47677,#47678,#47679,#47680),
 .UNSPECIFIED.,.F.,.F.,(4,4),(1.0915792594565,2.14101462431379),
 .UNSPECIFIED.);
#1213=B_SPLINE_CURVE_WITH_KNOTS('',3,(#47685,#47686,#47687,#47688),
 .UNSPECIFIED.,.F.,.F.,(4,4),(1.08247899997509,2.13195661716112),
 .UNSPECIFIED.);
#1214=B_SPLINE_CURVE_WITH_KNOTS('',3,(#47691,#47692,#47693,#47694),
 .UNSPECIFIED.,.F.,.F.,(4,4),(1.08711062908542,2.13658824627145),
 .UNSPECIFIED.);
#1215=B_SPLINE_CURVE_WITH_KNOTS('',3,(#47699,#47700,#47701,#47702),
 .UNSPECIFIED.,.F.,.F.,(4,4),(1.02489973343678,2.07455809562116),
 .UNSPECIFIED.);
#1216=B_SPLINE_CURVE_WITH_KNOTS('',3,(#47705,#47706,#47707,#47708),
 .UNSPECIFIED.,.F.,.F.,(4,4),(1.07188875891378,2.12154712109815),
 .UNSPECIFIED.);
#1217=B_SPLINE_CURVE_WITH_KNOTS('',3,(#47713,#47714,#47715,#47716),
 .UNSPECIFIED.,.F.,.F.,(4,4),(1.04935390711823,2.09892626486964),
 .UNSPECIFIED.);
#1218=B_SPLINE_CURVE_WITH_KNOTS('',3,(#47719,#47720,#47721,#47722),
 .UNSPECIFIED.,.F.,.F.,(4,4),(1.08048205057026,2.13005440832166),
 .UNSPECIFIED.);
#1219=B_SPLINE_CURVE_WITH_KNOTS('',3,(#47727,#47728,#47729,#47730),
 .UNSPECIFIED.,.F.,.F.,(4,4),(1.09744201858002,2.14688060738206),
 .UNSPECIFIED.);
#1220=B_SPLINE_CURVE_WITH_KNOTS('',3,(#47733,#47734,#47735,#47736),
 .UNSPECIFIED.,.F.,.F.,(4,4),(1.0908483826499,2.14028697145194),
 .UNSPECIFIED.);
#1221=B_SPLINE_CURVE_WITH_KNOTS('',3,(#47741,#47742,#47743,#47744),
 .UNSPECIFIED.,.F.,.F.,(4,4),(1.09579976662743,2.14524477934728),
 .UNSPECIFIED.);
#1222=B_SPLINE_CURVE_WITH_KNOTS('',3,(#47747,#47748,#47749,#47750),
 .UNSPECIFIED.,.F.,.F.,(4,4),(1.08939524602275,2.1388402587426),
 .UNSPECIFIED.);
#1223=B_SPLINE_CURVE_WITH_KNOTS('',3,(#47755,#47756,#47757,#47758),
 .UNSPECIFIED.,.F.,.F.,(4,4),(1.03575222205974,2.08537061780256),
 .UNSPECIFIED.);
#1224=B_SPLINE_CURVE_WITH_KNOTS('',3,(#47761,#47762,#47763,#47764),
 .UNSPECIFIED.,.F.,.F.,(4,4),(1.07627988374361,2.12589827948644),
 .UNSPECIFIED.);
#1225=B_SPLINE_CURVE_WITH_KNOTS('',3,(#47769,#47770,#47771,#47772),
 .UNSPECIFIED.,.F.,.F.,(4,4),(1.03575222205973,2.08537061780256),
 .UNSPECIFIED.);
#1226=B_SPLINE_CURVE_WITH_KNOTS('',3,(#47775,#47776,#47777,#47778),
 .UNSPECIFIED.,.F.,.F.,(4,4),(1.07627988374361,2.12589827948644),
 .UNSPECIFIED.);
#1227=B_SPLINE_CURVE_WITH_KNOTS('',3,(#47783,#47784,#47785,#47786),
 .UNSPECIFIED.,.F.,.F.,(4,4),(1.09579976662742,2.14524477934727),
 .UNSPECIFIED.);
#1228=B_SPLINE_CURVE_WITH_KNOTS('',3,(#47789,#47790,#47791,#47792),
 .UNSPECIFIED.,.F.,.F.,(4,4),(1.08939524602275,2.1388402587426),
 .UNSPECIFIED.);
#1229=B_SPLINE_CURVE_WITH_KNOTS('',3,(#47797,#47798,#47799,#47800),
 .UNSPECIFIED.,.F.,.F.,(4,4),(1.09744201858002,2.14688060738207),
 .UNSPECIFIED.);
#1230=B_SPLINE_CURVE_WITH_KNOTS('',3,(#47803,#47804,#47805,#47806),
 .UNSPECIFIED.,.F.,.F.,(4,4),(1.0908483826499,2.14028697145194),
 .UNSPECIFIED.);
#1231=B_SPLINE_CURVE_WITH_KNOTS('',3,(#47811,#47812,#47813,#47814),
 .UNSPECIFIED.,.F.,.F.,(4,4),(1.04935390711825,2.09892626486965),
 .UNSPECIFIED.);
#1232=B_SPLINE_CURVE_WITH_KNOTS('',3,(#47817,#47818,#47819,#47820),
 .UNSPECIFIED.,.F.,.F.,(4,4),(1.08048205057026,2.13005440832167),
 .UNSPECIFIED.);
#1233=B_SPLINE_CURVE_WITH_KNOTS('',3,(#47825,#47826,#47827,#47828),
 .UNSPECIFIED.,.F.,.F.,(4,4),(1.02489973343678,2.07455809562116),
 .UNSPECIFIED.);
#1234=B_SPLINE_CURVE_WITH_KNOTS('',3,(#47831,#47832,#47833,#47834),
 .UNSPECIFIED.,.F.,.F.,(4,4),(1.07188875891378,2.12154712109815),
 .UNSPECIFIED.);
#1235=B_SPLINE_CURVE_WITH_KNOTS('',3,(#47839,#47840,#47841,#47842),
 .UNSPECIFIED.,.F.,.F.,(4,4),(1.0824789999751,2.13195661716112),
 .UNSPECIFIED.);
#1236=B_SPLINE_CURVE_WITH_KNOTS('',3,(#47845,#47846,#47847,#47848),
 .UNSPECIFIED.,.F.,.F.,(4,4),(1.08711062908542,2.13658824627145),
 .UNSPECIFIED.);
#1237=B_SPLINE_CURVE_WITH_KNOTS('',3,(#47853,#47854,#47855,#47856),
 .UNSPECIFIED.,.F.,.F.,(4,4),(1.09826811479926,2.14770347965657),
 .UNSPECIFIED.);
#1238=B_SPLINE_CURVE_WITH_KNOTS('',3,(#47859,#47860,#47861,#47862),
 .UNSPECIFIED.,.F.,.F.,(4,4),(1.09157925945638,2.14101462431369),
 .UNSPECIFIED.);
#1239=B_SPLINE_CURVE_WITH_KNOTS('',3,(#47867,#47868,#47869,#47870),
 .UNSPECIFIED.,.F.,.F.,(4,4),(1.06516319055868,2.11468739222992),
 .UNSPECIFIED.);
#1240=B_SPLINE_CURVE_WITH_KNOTS('',3,(#47873,#47874,#47875,#47876),
 .UNSPECIFIED.,.F.,.F.,(4,4),(1.08410770108451,2.13363190275575),
 .UNSPECIFIED.);
#1241=B_SPLINE_CURVE_WITH_KNOTS('',3,(#47879,#47880,#47881,#47882),
 .UNSPECIFIED.,.F.,.F.,(4,4),(1.06604442753704,2.11573584316717),
 .UNSPECIFIED.);
#1242=B_SPLINE_CURVE_WITH_KNOTS('',3,(#47886,#47887,#47888,#47889),
 .UNSPECIFIED.,.F.,.F.,(4,4),(1.01713682798446,2.0668282436146),
 .UNSPECIFIED.);
#1243=B_SPLINE_CURVE_WITH_KNOTS('',3,(#47910,#47911,#47912,#47913),
 .UNSPECIFIED.,.F.,.F.,(4,4),(0.988228581953082,2.02619732383854),
 .UNSPECIFIED.);
#1244=B_SPLINE_CURVE_WITH_KNOTS('',3,(#47930,#47931,#47932,#47933),
 .UNSPECIFIED.,.F.,.F.,(4,4),(0.996245219772127,2.03408046027085),
 .UNSPECIFIED.);
#1245=B_SPLINE_CURVE_WITH_KNOTS('',3,(#47950,#47951,#47952,#47953),
 .UNSPECIFIED.,.F.,.F.,(4,4),(0.991257065987786,2.02917865590825),
 .UNSPECIFIED.);
#1246=B_SPLINE_CURVE_WITH_KNOTS('',3,(#47970,#47971,#47972,#47973),
 .UNSPECIFIED.,.F.,.F.,(4,4),(0.975946465952181,2.01405910333835),
 .UNSPECIFIED.);
#1247=B_SPLINE_CURVE_WITH_KNOTS('',3,(#47990,#47991,#47992,#47993),
 .UNSPECIFIED.,.F.,.F.,(4,4),(0.984583139670925,2.02260243625185),
 .UNSPECIFIED.);
#1248=B_SPLINE_CURVE_WITH_KNOTS('',3,(#48010,#48011,#48012,#48013),
 .UNSPECIFIED.,.F.,.F.,(4,4),(0.995299247716725,2.03315199866672),
 .UNSPECIFIED.);
#1249=B_SPLINE_CURVE_WITH_KNOTS('',3,(#48030,#48031,#48032,#48033),
 .UNSPECIFIED.,.F.,.F.,(4,4),(0.99362573826485,2.03150775762006),
 .UNSPECIFIED.);
#1250=B_SPLINE_CURVE_WITH_KNOTS('',3,(#48050,#48051,#48052,#48053),
 .UNSPECIFIED.,.F.,.F.,(4,4),(0.980365846111703,2.01843481385154),
 .UNSPECIFIED.);
#1251=B_SPLINE_CURVE_WITH_KNOTS('',3,(#48070,#48071,#48072,#48073),
 .UNSPECIFIED.,.F.,.F.,(4,4),(0.980365846111703,2.01843481385154),
 .UNSPECIFIED.);
#1252=B_SPLINE_CURVE_WITH_KNOTS('',3,(#48090,#48091,#48092,#48093),
 .UNSPECIFIED.,.F.,.F.,(4,4),(0.993625738264851,2.03150775762006),
 .UNSPECIFIED.);
#1253=B_SPLINE_CURVE_WITH_KNOTS('',3,(#48110,#48111,#48112,#48113),
 .UNSPECIFIED.,.F.,.F.,(4,4),(0.995299247716725,2.03315199866672),
 .UNSPECIFIED.);
#1254=B_SPLINE_CURVE_WITH_KNOTS('',3,(#48130,#48131,#48132,#48133),
 .UNSPECIFIED.,.F.,.F.,(4,4),(0.984583139670924,2.02260243625185),
 .UNSPECIFIED.);
#1255=B_SPLINE_CURVE_WITH_KNOTS('',3,(#48150,#48151,#48152,#48153),
 .UNSPECIFIED.,.F.,.F.,(4,4),(0.975946465952182,2.01405910333835),
 .UNSPECIFIED.);
#1256=B_SPLINE_CURVE_WITH_KNOTS('',3,(#48170,#48171,#48172,#48173),
 .UNSPECIFIED.,.F.,.F.,(4,4),(0.991257065987786,2.02917865590825),
 .UNSPECIFIED.);
#1257=B_SPLINE_CURVE_WITH_KNOTS('',3,(#48190,#48191,#48192,#48193),
 .UNSPECIFIED.,.F.,.F.,(4,4),(0.99624520912574,2.03408045013743),
 .UNSPECIFIED.);
#1258=B_SPLINE_CURVE_WITH_KNOTS('',3,(#48210,#48211,#48212,#48213),
 .UNSPECIFIED.,.F.,.F.,(4,4),(0.988228562594649,2.02619730816861),
 .UNSPECIFIED.);
#1259=B_SPLINE_CURVE_WITH_KNOTS('',3,(#48231,#48232,#48233,#48234),
 .UNSPECIFIED.,.F.,.F.,(4,4),(0.97041538436032,2.0085649015089),
 .UNSPECIFIED.);
#1260=B_SPLINE_CURVE_WITH_KNOTS('',3,(#48241,#48242,#48243,#48244),
 .UNSPECIFIED.,.F.,.F.,(4,4),(1.00572796764383,2.04369670952928),
 .UNSPECIFIED.);
#1261=B_SPLINE_CURVE_WITH_KNOTS('',3,(#48253,#48254,#48255,#48256),
 .UNSPECIFIED.,.F.,.F.,(4,4),(0.972542826498871,2.01061179423871),
 .UNSPECIFIED.);
#1262=B_SPLINE_CURVE_WITH_KNOTS('',3,(#48259,#48260,#48261,#48262),
 .UNSPECIFIED.,.F.,.F.,(4,4),(1.04725787168466,2.08513989103987),
 .UNSPECIFIED.);
#1263=B_SPLINE_CURVE_WITH_KNOTS('',3,(#48265,#48266,#48267,#48268),
 .UNSPECIFIED.,.F.,.F.,(4,4),(1.06889245483208,2.10674520578207),
 .UNSPECIFIED.);
#1264=B_SPLINE_CURVE_WITH_KNOTS('',3,(#48271,#48272,#48273,#48274),
 .UNSPECIFIED.,.F.,.F.,(4,4),(0.987740311273852,2.02575960785478),
 .UNSPECIFIED.);
#1265=B_SPLINE_CURVE_WITH_KNOTS('',3,(#48277,#48278,#48279,#48280),
 .UNSPECIFIED.,.F.,.F.,(4,4),(0.960726337881709,1.99883897526788),
 .UNSPECIFIED.);
#1266=B_SPLINE_CURVE_WITH_KNOTS('',3,(#48283,#48284,#48285,#48286),
 .UNSPECIFIED.,.F.,.F.,(4,4),(1.02588990754098,2.06381149746145),
 .UNSPECIFIED.);
#1267=B_SPLINE_CURVE_WITH_KNOTS('',3,(#48289,#48290,#48291,#48292),
 .UNSPECIFIED.,.F.,.F.,(4,4),(1.0893949973477,2.12723023784643),
 .UNSPECIFIED.);
#1268=B_SPLINE_CURVE_WITH_KNOTS('',3,(#48296,#48297,#48298,#48299),
 .UNSPECIFIED.,.F.,.F.,(4,4),(0.952533772491406,1.99068328963999),
 .UNSPECIFIED.);
#1269=B_SPLINE_CURVE_WITH_KNOTS('',3,(#48302,#48303,#48304,#48305),
 .UNSPECIFIED.,.F.,.F.,(4,4),(1.00572623032852,2.04369497590248),
 .UNSPECIFIED.);
#1270=B_SPLINE_CURVE_WITH_KNOTS('',3,(#48308,#48309,#48310,#48311),
 .UNSPECIFIED.,.F.,.F.,(4,4),(1.08939401792972,2.12722925894141),
 .UNSPECIFIED.);
#1271=B_SPLINE_CURVE_WITH_KNOTS('',3,(#48314,#48315,#48316,#48317),
 .UNSPECIFIED.,.F.,.F.,(4,4),(1.02588990754098,2.06381149746145),
 .UNSPECIFIED.);
#1272=B_SPLINE_CURVE_WITH_KNOTS('',3,(#48320,#48321,#48322,#48323),
 .UNSPECIFIED.,.F.,.F.,(4,4),(0.960726337881709,1.99883897526788),
 .UNSPECIFIED.);
#1273=B_SPLINE_CURVE_WITH_KNOTS('',3,(#48326,#48327,#48328,#48329),
 .UNSPECIFIED.,.F.,.F.,(4,4),(0.987740311273852,2.02575960785478),
 .UNSPECIFIED.);
#1274=B_SPLINE_CURVE_WITH_KNOTS('',3,(#48332,#48333,#48334,#48335),
 .UNSPECIFIED.,.F.,.F.,(4,4),(1.06889245483208,2.10674520578207),
 .UNSPECIFIED.);
#1275=B_SPLINE_CURVE_WITH_KNOTS('',3,(#48338,#48339,#48340,#48341),
 .UNSPECIFIED.,.F.,.F.,(4,4),(1.04725787168466,2.08513989103987),
 .UNSPECIFIED.);
#1276=B_SPLINE_CURVE_WITH_KNOTS('',3,(#48344,#48345,#48346,#48347),
 .UNSPECIFIED.,.F.,.F.,(4,4),(0.972542826498871,2.01061179423871),
 .UNSPECIFIED.);
#1523=SHAPE_REPRESENTATION_RELATIONSHIP('SRR','None',#59312,#1543);
#1543=ADVANCED_BREP_SHAPE_REPRESENTATION('',(#1590),#59199);
#1570=STYLED_ITEM('',(#59586),#1590);
#1590=MANIFOLD_SOLID_BREP('Cone assembly',#22819);
#1758=FACE_BOUND('',#5014,.T.);
#1759=FACE_BOUND('',#5015,.T.);
#1760=FACE_BOUND('',#5016,.T.);
#1761=FACE_BOUND('',#5017,.T.);
#1762=FACE_BOUND('',#5018,.T.);
#1763=FACE_BOUND('',#5019,.T.);
#1764=FACE_BOUND('',#5020,.T.);
#1765=FACE_BOUND('',#5021,.T.);
#1766=FACE_BOUND('',#5022,.T.);
#1767=FACE_BOUND('',#5023,.T.);
#1768=FACE_BOUND('',#5024,.T.);
#1769=FACE_BOUND('',#5025,.T.);
#1770=FACE_BOUND('',#5026,.T.);
#1771=FACE_BOUND('',#5027,.T.);
#1772=FACE_BOUND('',#5028,.T.);
#1773=FACE_BOUND('',#5029,.T.);
#1774=FACE_BOUND('',#5030,.T.);
#1775=FACE_BOUND('',#5032,.T.);
#1776=FACE_BOUND('',#5033,.T.);
#1777=FACE_BOUND('',#5034,.T.);
#1778=FACE_BOUND('',#5035,.T.);
#1779=FACE_BOUND('',#5036,.T.);
#1780=FACE_BOUND('',#5037,.T.);
#1781=FACE_BOUND('',#5038,.T.);
#1782=FACE_BOUND('',#5039,.T.);
#1783=FACE_BOUND('',#5040,.T.);
#1784=FACE_BOUND('',#5041,.T.);
#1785=FACE_BOUND('',#5042,.T.);
#1786=FACE_BOUND('',#5043,.T.);
#1787=FACE_BOUND('',#5044,.T.);
#1788=FACE_BOUND('',#5045,.T.);
#1789=FACE_BOUND('',#5046,.T.);
#1790=FACE_BOUND('',#5047,.T.);
#1791=FACE_BOUND('',#5048,.T.);
#1792=FACE_BOUND('',#5173,.T.);
#1793=FACE_BOUND('',#5177,.T.);
#1794=FACE_BOUND('',#5179,.T.);
#1795=FACE_BOUND('',#5182,.T.);
#2158=PLANE('',#24308);
#2159=PLANE('',#24310);
#2160=PLANE('',#24319);
#2161=PLANE('',#24320);
#2162=PLANE('',#24322);
#2163=PLANE('',#24331);
#2164=PLANE('',#24332);
#2165=PLANE('',#24334);
#2166=PLANE('',#24343);
#2167=PLANE('',#24344);
#2168=PLANE('',#24346);
#2169=PLANE('',#24355);
#2170=PLANE('',#24356);
#2171=PLANE('',#24358);
#2172=PLANE('',#24367);
#2173=PLANE('',#24368);
#2174=PLANE('',#24370);
#2175=PLANE('',#24379);
#2176=PLANE('',#24380);
#2177=PLANE('',#24382);
#2178=PLANE('',#24391);
#2179=PLANE('',#24392);
#2180=PLANE('',#24394);
#2181=PLANE('',#24403);
#2182=PLANE('',#24404);
#2183=PLANE('',#24406);
#2184=PLANE('',#24415);
#2185=PLANE('',#24416);
#2186=PLANE('',#24418);
#2187=PLANE('',#24427);
#2188=PLANE('',#24428);
#2189=PLANE('',#24430);
#2190=PLANE('',#24439);
#2191=PLANE('',#24440);
#2192=PLANE('',#24442);
#2193=PLANE('',#24451);
#2194=PLANE('',#24452);
#2195=PLANE('',#24454);
#2196=PLANE('',#24463);
#2197=PLANE('',#24464);
#2198=PLANE('',#24466);
#2199=PLANE('',#24475);
#2200=PLANE('',#24476);
#2201=PLANE('',#24478);
#2202=PLANE('',#24487);
#2203=PLANE('',#24488);
#2204=PLANE('',#24490);
#2205=PLANE('',#24499);
#2206=PLANE('',#24500);
#2207=PLANE('',#24502);
#2208=PLANE('',#24504);
#2209=PLANE('',#24512);
#2210=PLANE('',#24536);
#2211=PLANE('',#24540);
#2212=PLANE('',#24544);
#2213=PLANE('',#24548);
#2214=PLANE('',#24552);
#2215=PLANE('',#24556);
#2216=PLANE('',#24560);
#2217=PLANE('',#24564);
#2218=PLANE('',#24568);
#2219=PLANE('',#24572);
#2220=PLANE('',#24576);
#2221=PLANE('',#24580);
#2222=PLANE('',#24584);
#2223=PLANE('',#24588);
#2224=PLANE('',#24592);
#2225=PLANE('',#24599);
#2226=PLANE('',#24603);
#2227=PLANE('',#24609);
#2228=PLANE('',#24610);
#2229=PLANE('',#24614);
#2579=CYLINDRICAL_SURFACE('',#24607,1.9);
#2580=CYLINDRICAL_SURFACE('',#24612,1.6);
#2581=CYLINDRICAL_SURFACE('',#24618,1.25);
#3549=FACE_OUTER_BOUND('',#5013,.T.);
#3550=FACE_OUTER_BOUND('',#5031,.T.);
#3551=FACE_OUTER_BOUND('',#5049,.T.);
#3552=FACE_OUTER_BOUND('',#5050,.T.);
#3553=FACE_OUTER_BOUND('',#5051,.T.);
#3554=FACE_OUTER_BOUND('',#5052,.T.);
#3555=FACE_OUTER_BOUND('',#5053,.T.);
#3556=FACE_OUTER_BOUND('',#5054,.T.);
#3557=FACE_OUTER_BOUND('',#5055,.T.);
#3558=FACE_OUTER_BOUND('',#5056,.T.);
#3559=FACE_OUTER_BOUND('',#5057,.T.);
#3560=FACE_OUTER_BOUND('',#5058,.T.);
#3561=FACE_OUTER_BOUND('',#5059,.T.);
#3562=FACE_OUTER_BOUND('',#5060,.T.);
#3563=FACE_OUTER_BOUND('',#5061,.T.);
#3564=FACE_OUTER_BOUND('',#5062,.T.);
#3565=FACE_OUTER_BOUND('',#5063,.T.);
#3566=FACE_OUTER_BOUND('',#5064,.T.);
#3567=FACE_OUTER_BOUND('',#5065,.T.);
#3568=FACE_OUTER_BOUND('',#5066,.T.);
#3569=FACE_OUTER_BOUND('',#5067,.T.);
#3570=FACE_OUTER_BOUND('',#5068,.T.);
#3571=FACE_OUTER_BOUND('',#5069,.T.);
#3572=FACE_OUTER_BOUND('',#5070,.T.);
#3573=FACE_OUTER_BOUND('',#5071,.T.);
#3574=FACE_OUTER_BOUND('',#5072,.T.);
#3575=FACE_OUTER_BOUND('',#5073,.T.);
#3576=FACE_OUTER_BOUND('',#5074,.T.);
#3577=FACE_OUTER_BOUND('',#5075,.T.);
#3578=FACE_OUTER_BOUND('',#5076,.T.);
#3579=FACE_OUTER_BOUND('',#5077,.T.);
#3580=FACE_OUTER_BOUND('',#5078,.T.);
#3581=FACE_OUTER_BOUND('',#5079,.T.);
#3582=FACE_OUTER_BOUND('',#5080,.T.);
#3583=FACE_OUTER_BOUND('',#5081,.T.);
#3584=FACE_OUTER_BOUND('',#5082,.T.);
#3585=FACE_OUTER_BOUND('',#5083,.T.);
#3586=FACE_OUTER_BOUND('',#5084,.T.);
#3587=FACE_OUTER_BOUND('',#5085,.T.);
#3588=FACE_OUTER_BOUND('',#5086,.T.);
#3589=FACE_OUTER_BOUND('',#5087,.T.);
#3590=FACE_OUTER_BOUND('',#5088,.T.);
#3591=FACE_OUTER_BOUND('',#5089,.T.);
#3592=FACE_OUTER_BOUND('',#5090,.T.);
#3593=FACE_OUTER_BOUND('',#5091,.T.);
#3594=FACE_OUTER_BOUND('',#5092,.T.);
#3595=FACE_OUTER_BOUND('',#5093,.T.);
#3596=FACE_OUTER_BOUND('',#5094,.T.);
#3597=FACE_OUTER_BOUND('',#5095,.T.);
#3598=FACE_OUTER_BOUND('',#5096,.T.);
#3599=FACE_OUTER_BOUND('',#5097,.T.);
#3600=FACE_OUTER_BOUND('',#5098,.T.);
#3601=FACE_OUTER_BOUND('',#5099,.T.);
#3602=FACE_OUTER_BOUND('',#5100,.T.);
#3603=FACE_OUTER_BOUND('',#5101,.T.);
#3604=FACE_OUTER_BOUND('',#5102,.T.);
#3605=FACE_OUTER_BOUND('',#5103,.T.);
#3606=FACE_OUTER_BOUND('',#5104,.T.);
#3607=FACE_OUTER_BOUND('',#5105,.T.);
#3608=FACE_OUTER_BOUND('',#5106,.T.);
#3609=FACE_OUTER_BOUND('',#5107,.T.);
#3610=FACE_OUTER_BOUND('',#5108,.T.);
#3611=FACE_OUTER_BOUND('',#5109,.T.);
#3612=FACE_OUTER_BOUND('',#5110,.T.);
#3613=FACE_OUTER_BOUND('',#5111,.T.);
#3614=FACE_OUTER_BOUND('',#5112,.T.);
#3615=FACE_OUTER_BOUND('',#5113,.T.);
#3616=FACE_OUTER_BOUND('',#5114,.T.);
#3617=FACE_OUTER_BOUND('',#5115,.T.);
#3618=FACE_OUTER_BOUND('',#5116,.T.);
#3619=FACE_OUTER_BOUND('',#5117,.T.);
#3620=FACE_OUTER_BOUND('',#5118,.T.);
#3621=FACE_OUTER_BOUND('',#5119,.T.);
#3622=FACE_OUTER_BOUND('',#5120,.T.);
#3623=FACE_OUTER_BOUND('',#5121,.T.);
#3624=FACE_OUTER_BOUND('',#5122,.T.);
#3625=FACE_OUTER_BOUND('',#5123,.T.);
#3626=FACE_OUTER_BOUND('',#5124,.T.);
#3627=FACE_OUTER_BOUND('',#5125,.T.);
#3628=FACE_OUTER_BOUND('',#5126,.T.);
#3629=FACE_OUTER_BOUND('',#5127,.T.);
#3630=FACE_OUTER_BOUND('',#5128,.T.);
#3631=FACE_OUTER_BOUND('',#5129,.T.);
#3632=FACE_OUTER_BOUND('',#5130,.T.);
#3633=FACE_OUTER_BOUND('',#5131,.T.);
#3634=FACE_OUTER_BOUND('',#5132,.T.);
#3635=FACE_OUTER_BOUND('',#5133,.T.);
#3636=FACE_OUTER_BOUND('',#5134,.T.);
#3637=FACE_OUTER_BOUND('',#5135,.T.);
#3638=FACE_OUTER_BOUND('',#5136,.T.);
#3639=FACE_OUTER_BOUND('',#5137,.T.);
#3640=FACE_OUTER_BOUND('',#5138,.T.);
#3641=FACE_OUTER_BOUND('',#5139,.T.);
#3642=FACE_OUTER_BOUND('',#5140,.T.);
#3643=FACE_OUTER_BOUND('',#5141,.T.);
#3644=FACE_OUTER_BOUND('',#5142,.T.);
#3645=FACE_OUTER_BOUND('',#5143,.T.);
#3646=FACE_OUTER_BOUND('',#5144,.T.);
#3647=FACE_OUTER_BOUND('',#5145,.T.);
#3648=FACE_OUTER_BOUND('',#5146,.T.);
#3649=FACE_OUTER_BOUND('',#5147,.T.);
#3650=FACE_OUTER_BOUND('',#5148,.T.);
#3651=FACE_OUTER_BOUND('',#5149,.T.);
#3652=FACE_OUTER_BOUND('',#5150,.T.);
#3653=FACE_OUTER_BOUND('',#5151,.T.);
#3654=FACE_OUTER_BOUND('',#5152,.T.);
#3655=FACE_OUTER_BOUND('',#5153,.T.);
#3656=FACE_OUTER_BOUND('',#5154,.T.);
#3657=FACE_OUTER_BOUND('',#5155,.T.);
#3658=FACE_OUTER_BOUND('',#5156,.T.);
#3659=FACE_OUTER_BOUND('',#5157,.T.);
#3660=FACE_OUTER_BOUND('',#5158,.T.);
#3661=FACE_OUTER_BOUND('',#5159,.T.);
#3662=FACE_OUTER_BOUND('',#5160,.T.);
#3663=FACE_OUTER_BOUND('',#5161,.T.);
#3664=FACE_OUTER_BOUND('',#5162,.T.);
#3665=FACE_OUTER_BOUND('',#5163,.T.);
#3666=FACE_OUTER_BOUND('',#5164,.T.);
#3667=FACE_OUTER_BOUND('',#5165,.T.);
#3668=FACE_OUTER_BOUND('',#5166,.T.);
#3669=FACE_OUTER_BOUND('',#5167,.T.);
#3670=FACE_OUTER_BOUND('',#5168,.T.);
#3671=FACE_OUTER_BOUND('',#5169,.T.);
#3672=FACE_OUTER_BOUND('',#5170,.T.);
#3673=FACE_OUTER_BOUND('',#5171,.T.);
#3674=FACE_OUTER_BOUND('',#5172,.T.);
#3675=FACE_OUTER_BOUND('',#5174,.T.);
#3676=FACE_OUTER_BOUND('',#5175,.T.);
#3677=FACE_OUTER_BOUND('',#5176,.T.);
#3678=FACE_OUTER_BOUND('',#5178,.T.);
#3679=FACE_OUTER_BOUND('',#5180,.T.);
#3680=FACE_OUTER_BOUND('',#5181,.T.);
#3681=FACE_OUTER_BOUND('',#5183,.T.);
#3682=FACE_OUTER_BOUND('',#5184,.T.);
#5013=EDGE_LOOP('',(#19068,#19069,#19070,#19071));
#5014=EDGE_LOOP('',(#19072,#19073,#19074,#19075));
#5015=EDGE_LOOP('',(#19076,#19077,#19078,#19079));
#5016=EDGE_LOOP('',(#19080,#19081,#19082,#19083));
#5017=EDGE_LOOP('',(#19084,#19085,#19086,#19087));
#5018=EDGE_LOOP('',(#19088,#19089,#19090,#19091));
#5019=EDGE_LOOP('',(#19092,#19093,#19094,#19095));
#5020=EDGE_LOOP('',(#19096,#19097,#19098,#19099));
#5021=EDGE_LOOP('',(#19100,#19101,#19102,#19103));
#5022=EDGE_LOOP('',(#19104,#19105,#19106,#19107));
#5023=EDGE_LOOP('',(#19108,#19109,#19110,#19111));
#5024=EDGE_LOOP('',(#19112,#19113,#19114,#19115));
#5025=EDGE_LOOP('',(#19116,#19117,#19118,#19119));
#5026=EDGE_LOOP('',(#19120,#19121,#19122,#19123));
#5027=EDGE_LOOP('',(#19124,#19125,#19126,#19127));
#5028=EDGE_LOOP('',(#19128,#19129,#19130,#19131));
#5029=EDGE_LOOP('',(#19132,#19133,#19134,#19135));
#5030=EDGE_LOOP('',(#19136,#19137,#19138,#19139));
#5031=EDGE_LOOP('',(#19140,#19141,#19142,#19143));
#5032=EDGE_LOOP('',(#19144,#19145,#19146,#19147));
#5033=EDGE_LOOP('',(#19148,#19149,#19150,#19151));
#5034=EDGE_LOOP('',(#19152,#19153,#19154,#19155));
#5035=EDGE_LOOP('',(#19156,#19157,#19158,#19159));
#5036=EDGE_LOOP('',(#19160,#19161,#19162,#19163));
#5037=EDGE_LOOP('',(#19164,#19165,#19166,#19167));
#5038=EDGE_LOOP('',(#19168,#19169,#19170,#19171));
#5039=EDGE_LOOP('',(#19172,#19173,#19174,#19175));
#5040=EDGE_LOOP('',(#19176,#19177,#19178,#19179));
#5041=EDGE_LOOP('',(#19180,#19181,#19182,#19183));
#5042=EDGE_LOOP('',(#19184,#19185,#19186,#19187));
#5043=EDGE_LOOP('',(#19188,#19189,#19190,#19191));
#5044=EDGE_LOOP('',(#19192,#19193,#19194,#19195));
#5045=EDGE_LOOP('',(#19196,#19197,#19198,#19199));
#5046=EDGE_LOOP('',(#19200,#19201,#19202,#19203));
#5047=EDGE_LOOP('',(#19204,#19205,#19206,#19207));
#5048=EDGE_LOOP('',(#19208,#19209,#19210,#19211));
#5049=EDGE_LOOP('',(#19212,#19213,#19214,#19215));
#5050=EDGE_LOOP('',(#19216,#19217,#19218,#19219));
#5051=EDGE_LOOP('',(#19220,#19221));
#5052=EDGE_LOOP('',(#19222,#19223,#19224,#19225));
#5053=EDGE_LOOP('',(#19226,#19227,#19228,#19229));
#5054=EDGE_LOOP('',(#19230,#19231,#19232,#19233,#19234));
#5055=EDGE_LOOP('',(#19235,#19236));
#5056=EDGE_LOOP('',(#19237,#19238));
#5057=EDGE_LOOP('',(#19239,#19240,#19241,#19242));
#5058=EDGE_LOOP('',(#19243,#19244,#19245,#19246));
#5059=EDGE_LOOP('',(#19247,#19248,#19249,#19250,#19251));
#5060=EDGE_LOOP('',(#19252,#19253));
#5061=EDGE_LOOP('',(#19254,#19255));
#5062=EDGE_LOOP('',(#19256,#19257,#19258,#19259));
#5063=EDGE_LOOP('',(#19260,#19261,#19262,#19263));
#5064=EDGE_LOOP('',(#19264,#19265,#19266,#19267,#19268));
#5065=EDGE_LOOP('',(#19269,#19270));
#5066=EDGE_LOOP('',(#19271,#19272));
#5067=EDGE_LOOP('',(#19273,#19274,#19275,#19276));
#5068=EDGE_LOOP('',(#19277,#19278,#19279,#19280));
#5069=EDGE_LOOP('',(#19281,#19282,#19283,#19284,#19285));
#5070=EDGE_LOOP('',(#19286,#19287));
#5071=EDGE_LOOP('',(#19288,#19289));
#5072=EDGE_LOOP('',(#19290,#19291,#19292,#19293));
#5073=EDGE_LOOP('',(#19294,#19295,#19296,#19297));
#5074=EDGE_LOOP('',(#19298,#19299,#19300,#19301,#19302));
#5075=EDGE_LOOP('',(#19303,#19304));
#5076=EDGE_LOOP('',(#19305,#19306));
#5077=EDGE_LOOP('',(#19307,#19308,#19309,#19310));
#5078=EDGE_LOOP('',(#19311,#19312,#19313,#19314));
#5079=EDGE_LOOP('',(#19315,#19316,#19317,#19318,#19319));
#5080=EDGE_LOOP('',(#19320,#19321));
#5081=EDGE_LOOP('',(#19322,#19323));
#5082=EDGE_LOOP('',(#19324,#19325,#19326,#19327));
#5083=EDGE_LOOP('',(#19328,#19329,#19330,#19331));
#5084=EDGE_LOOP('',(#19332,#19333,#19334,#19335,#19336));
#5085=EDGE_LOOP('',(#19337,#19338));
#5086=EDGE_LOOP('',(#19339,#19340));
#5087=EDGE_LOOP('',(#19341,#19342,#19343,#19344));
#5088=EDGE_LOOP('',(#19345,#19346,#19347,#19348));
#5089=EDGE_LOOP('',(#19349,#19350,#19351,#19352,#19353));
#5090=EDGE_LOOP('',(#19354,#19355));
#5091=EDGE_LOOP('',(#19356,#19357));
#5092=EDGE_LOOP('',(#19358,#19359,#19360,#19361));
#5093=EDGE_LOOP('',(#19362,#19363,#19364,#19365));
#5094=EDGE_LOOP('',(#19366,#19367,#19368,#19369,#19370));
#5095=EDGE_LOOP('',(#19371,#19372));
#5096=EDGE_LOOP('',(#19373,#19374));
#5097=EDGE_LOOP('',(#19375,#19376,#19377,#19378));
#5098=EDGE_LOOP('',(#19379,#19380,#19381,#19382));
#5099=EDGE_LOOP('',(#19383,#19384,#19385,#19386,#19387));
#5100=EDGE_LOOP('',(#19388,#19389));
#5101=EDGE_LOOP('',(#19390,#19391));
#5102=EDGE_LOOP('',(#19392,#19393,#19394,#19395));
#5103=EDGE_LOOP('',(#19396,#19397,#19398,#19399));
#5104=EDGE_LOOP('',(#19400,#19401,#19402,#19403,#19404));
#5105=EDGE_LOOP('',(#19405,#19406));
#5106=EDGE_LOOP('',(#19407,#19408));
#5107=EDGE_LOOP('',(#19409,#19410,#19411,#19412));
#5108=EDGE_LOOP('',(#19413,#19414,#19415,#19416));
#5109=EDGE_LOOP('',(#19417,#19418,#19419,#19420,#19421));
#5110=EDGE_LOOP('',(#19422,#19423));
#5111=EDGE_LOOP('',(#19424,#19425));
#5112=EDGE_LOOP('',(#19426,#19427,#19428,#19429));
#5113=EDGE_LOOP('',(#19430,#19431,#19432,#19433));
#5114=EDGE_LOOP('',(#19434,#19435,#19436,#19437,#19438));
#5115=EDGE_LOOP('',(#19439,#19440));
#5116=EDGE_LOOP('',(#19441,#19442));
#5117=EDGE_LOOP('',(#19443,#19444,#19445,#19446));
#5118=EDGE_LOOP('',(#19447,#19448,#19449,#19450));
#5119=EDGE_LOOP('',(#19451,#19452,#19453,#19454,#19455));
#5120=EDGE_LOOP('',(#19456,#19457));
#5121=EDGE_LOOP('',(#19458,#19459));
#5122=EDGE_LOOP('',(#19460,#19461,#19462,#19463));
#5123=EDGE_LOOP('',(#19464,#19465,#19466,#19467));
#5124=EDGE_LOOP('',(#19468,#19469,#19470,#19471,#19472));
#5125=EDGE_LOOP('',(#19473,#19474));
#5126=EDGE_LOOP('',(#19475,#19476));
#5127=EDGE_LOOP('',(#19477,#19478,#19479,#19480));
#5128=EDGE_LOOP('',(#19481,#19482,#19483,#19484));
#5129=EDGE_LOOP('',(#19485,#19486,#19487,#19488,#19489));
#5130=EDGE_LOOP('',(#19490,#19491));
#5131=EDGE_LOOP('',(#19492,#19493));
#5132=EDGE_LOOP('',(#19494,#19495));
#5133=EDGE_LOOP('',(#19496,#19497,#19498,#19499));
#5134=EDGE_LOOP('',(#19500,#19501,#19502,#19503));
#5135=EDGE_LOOP('',(#19504,#19505,#19506,#19507,#19508));
#5136=EDGE_LOOP('',(#19509,#19510,#19511,#19512));
#5137=EDGE_LOOP('',(#19513,#19514,#19515,#19516,#19517));
#5138=EDGE_LOOP('',(#19518,#19519,#19520,#19521,#19522,#19523,#19524,#19525,
#19526,#19527,#19528,#19529,#19530,#19531,#19532,#19533,#19534,#19535,#19536,
#19537,#19538,#19539,#19540,#19541,#19542,#19543,#19544,#19545,#19546,#19547,
#19548,#19549,#19550,#19551,#19552,#19553,#19554,#19555,#19556,#19557,#19558,
#19559,#19560,#19561,#19562,#19563,#19564,#19565,#19566,#19567,#19568,#19569,
#19570,#19571,#19572,#19573,#19574,#19575,#19576,#19577,#19578,#19579,#19580,
#19581,#19582,#19583,#19584,#19585,#19586,#19587,#19588,#19589));
#5139=EDGE_LOOP('',(#19590,#19591,#19592,#19593));
#5140=EDGE_LOOP('',(#19594,#19595,#19596,#19597,#19598));
#5141=EDGE_LOOP('',(#19599,#19600,#19601,#19602));
#5142=EDGE_LOOP('',(#19603,#19604,#19605,#19606,#19607));
#5143=EDGE_LOOP('',(#19608,#19609,#19610,#19611));
#5144=EDGE_LOOP('',(#19612,#19613,#19614,#19615,#19616));
#5145=EDGE_LOOP('',(#19617,#19618,#19619,#19620));
#5146=EDGE_LOOP('',(#19621,#19622,#19623,#19624,#19625));
#5147=EDGE_LOOP('',(#19626,#19627,#19628,#19629));
#5148=EDGE_LOOP('',(#19630,#19631,#19632,#19633,#19634));
#5149=EDGE_LOOP('',(#19635,#19636,#19637,#19638));
#5150=EDGE_LOOP('',(#19639,#19640,#19641,#19642,#19643));
#5151=EDGE_LOOP('',(#19644,#19645,#19646,#19647));
#5152=EDGE_LOOP('',(#19648,#19649,#19650,#19651,#19652));
#5153=EDGE_LOOP('',(#19653,#19654,#19655,#19656));
#5154=EDGE_LOOP('',(#19657,#19658,#19659,#19660,#19661));
#5155=EDGE_LOOP('',(#19662,#19663,#19664,#19665));
#5156=EDGE_LOOP('',(#19666,#19667,#19668,#19669,#19670));
#5157=EDGE_LOOP('',(#19671,#19672,#19673,#19674));
#5158=EDGE_LOOP('',(#19675,#19676,#19677,#19678,#19679));
#5159=EDGE_LOOP('',(#19680,#19681,#19682,#19683));
#5160=EDGE_LOOP('',(#19684,#19685,#19686,#19687,#19688));
#5161=EDGE_LOOP('',(#19689,#19690,#19691,#19692));
#5162=EDGE_LOOP('',(#19693,#19694,#19695,#19696,#19697));
#5163=EDGE_LOOP('',(#19698,#19699,#19700,#19701));
#5164=EDGE_LOOP('',(#19702,#19703,#19704,#19705,#19706));
#5165=EDGE_LOOP('',(#19707,#19708,#19709,#19710));
#5166=EDGE_LOOP('',(#19711,#19712,#19713,#19714,#19715));
#5167=EDGE_LOOP('',(#19716,#19717,#19718,#19719));
#5168=EDGE_LOOP('',(#19720,#19721,#19722,#19723,#19724));
#5169=EDGE_LOOP('',(#19725,#19726,#19727,#19728,#19729));
#5170=EDGE_LOOP('',(#19730,#19731,#19732,#19733));
#5171=EDGE_LOOP('',(#19734,#19735,#19736,#19737));
#5172=EDGE_LOOP('',(#19738));
#5173=EDGE_LOOP('',(#19739));
#5174=EDGE_LOOP('',(#19740,#19741,#19742,#19743));
#5175=EDGE_LOOP('',(#19744,#19745,#19746,#19747));
#5176=EDGE_LOOP('',(#19748));
#5177=EDGE_LOOP('',(#19749,#19750,#19751,#19752,#19753,#19754,#19755,#19756,
#19757,#19758,#19759,#19760,#19761,#19762,#19763,#19764,#19765,#19766,#19767,
#19768,#19769,#19770,#19771,#19772,#19773,#19774,#19775,#19776,#19777,#19778,
#19779,#19780,#19781,#19782,#19783,#19784,#19785,#19786,#19787,#19788,#19789,
#19790,#19791,#19792,#19793,#19794,#19795,#19796,#19797,#19798,#19799,#19800,
#19801,#19802,#19803,#19804,#19805,#19806,#19807,#19808,#19809,#19810,#19811,
#19812,#19813,#19814,#19815,#19816,#19817));
#5178=EDGE_LOOP('',(#19818));
#5179=EDGE_LOOP('',(#19819));
#5180=EDGE_LOOP('',(#19820,#19821,#19822,#19823));
#5181=EDGE_LOOP('',(#19824));
#5182=EDGE_LOOP('',(#19825));
#5183=EDGE_LOOP('',(#19826,#19827,#19828,#19829));
#5184=EDGE_LOOP('',(#19830,#19831,#19832,#19833));
#6510=LINE('',#47407,#7943);
#6511=LINE('',#47651,#7944);
#6512=LINE('',#47892,#7945);
#6513=LINE('',#47894,#7946);
#6514=LINE('',#48238,#7947);
#6515=LINE('',#48250,#7948);
#6516=LINE('',#48352,#7949);
#6517=LINE('',#48358,#7950);
#6518=LINE('',#48364,#7951);
#6519=LINE('',#48370,#7952);
#6520=LINE('',#48376,#7953);
#6521=LINE('',#48382,#7954);
#6522=LINE('',#48388,#7955);
#6523=LINE('',#48394,#7956);
#6524=LINE('',#48400,#7957);
#6525=LINE('',#48406,#7958);
#6526=LINE('',#48412,#7959);
#6527=LINE('',#48418,#7960);
#6528=LINE('',#48424,#7961);
#6529=LINE('',#48430,#7962);
#6530=LINE('',#48436,#7963);
#6531=LINE('',#48444,#7964);
#6532=LINE('',#48449,#7965);
#6533=LINE('',#48457,#7966);
#6534=LINE('',#48461,#7967);
#6535=LINE('',#48469,#7968);
#6536=LINE('',#48475,#7969);
#6537=LINE('',#48478,#7970);
#7943=VECTOR('',#28514,1.88899277133291);
#7944=VECTOR('',#28589,1.96724457939162);
#7945=VECTOR('',#28662,2.06222171593972);
#7946=VECTOR('',#28665,1.79401563478481);
#7947=VECTOR('',#29078,1.);
#7948=VECTOR('',#29087,1.61107777577792);
#7949=VECTOR('',#29128,1.);
#7950=VECTOR('',#29137,1.);
#7951=VECTOR('',#29146,1.);
#7952=VECTOR('',#29155,1.);
#7953=VECTOR('',#29164,1.);
#7954=VECTOR('',#29173,1.);
#7955=VECTOR('',#29182,1.);
#7956=VECTOR('',#29191,1.);
#7957=VECTOR('',#29200,1.);
#7958=VECTOR('',#29209,1.);
#7959=VECTOR('',#29218,1.);
#7960=VECTOR('',#29227,1.);
#7961=VECTOR('',#29236,1.);
#7962=VECTOR('',#29245,1.);
#7963=VECTOR('',#29254,1.);
#7964=VECTOR('',#29267,1.);
#7965=VECTOR('',#29272,1.28);
#7966=VECTOR('',#29283,1.87);
#7967=VECTOR('',#29288,1.9);
#7968=VECTOR('',#29299,1.6);
#7969=VECTOR('',#29306,1.28);
#7970=VECTOR('',#29311,1.25);
#8891=CIRCLE('',#24233,1.75488973075546);
#8892=CIRCLE('',#24234,2.02309581191037);
#8893=CIRCLE('',#24270,1.83314153881416);
#8894=CIRCLE('',#24271,2.10134761996907);
#8895=CIRCLE('',#24309,0.3);
#8896=CIRCLE('',#24311,0.3);
#8897=CIRCLE('',#24313,0.3);
#8898=CIRCLE('',#24315,0.34);
#8899=CIRCLE('',#24317,0.34);
#8900=CIRCLE('',#24321,0.3);
#8901=CIRCLE('',#24323,0.3);
#8902=CIRCLE('',#24325,0.3);
#8903=CIRCLE('',#24327,0.34);
#8904=CIRCLE('',#24329,0.34);
#8905=CIRCLE('',#24333,0.3);
#8906=CIRCLE('',#24335,0.3);
#8907=CIRCLE('',#24337,0.3);
#8908=CIRCLE('',#24339,0.34);
#8909=CIRCLE('',#24341,0.34);
#8910=CIRCLE('',#24345,0.3);
#8911=CIRCLE('',#24347,0.3);
#8912=CIRCLE('',#24349,0.3);
#8913=CIRCLE('',#24351,0.34);
#8914=CIRCLE('',#24353,0.34);
#8915=CIRCLE('',#24357,0.3);
#8916=CIRCLE('',#24359,0.3);
#8917=CIRCLE('',#24361,0.3);
#8918=CIRCLE('',#24363,0.34);
#8919=CIRCLE('',#24365,0.34);
#8920=CIRCLE('',#24369,0.3);
#8921=CIRCLE('',#24371,0.3);
#8922=CIRCLE('',#24373,0.3);
#8923=CIRCLE('',#24375,0.34);
#8924=CIRCLE('',#24377,0.34);
#8925=CIRCLE('',#24381,0.3);
#8926=CIRCLE('',#24383,0.3);
#8927=CIRCLE('',#24385,0.3);
#8928=CIRCLE('',#24387,0.34);
#8929=CIRCLE('',#24389,0.34);
#8930=CIRCLE('',#24393,0.3);
#8931=CIRCLE('',#24395,0.3);
#8932=CIRCLE('',#24397,0.3);
#8933=CIRCLE('',#24399,0.34);
#8934=CIRCLE('',#24401,0.34);
#8935=CIRCLE('',#24405,0.3);
#8936=CIRCLE('',#24407,0.3);
#8937=CIRCLE('',#24409,0.3);
#8938=CIRCLE('',#24411,0.34);
#8939=CIRCLE('',#24413,0.34);
#8940=CIRCLE('',#24417,0.3);
#8941=CIRCLE('',#24419,0.3);
#8942=CIRCLE('',#24421,0.3);
#8943=CIRCLE('',#24423,0.34);
#8944=CIRCLE('',#24425,0.34);
#8945=CIRCLE('',#24429,0.3);
#8946=CIRCLE('',#24431,0.3);
#8947=CIRCLE('',#24433,0.3);
#8948=CIRCLE('',#24435,0.34);
#8949=CIRCLE('',#24437,0.34);
#8950=CIRCLE('',#24441,0.3);
#8951=CIRCLE('',#24443,0.3);
#8952=CIRCLE('',#24445,0.3);
#8953=CIRCLE('',#24447,0.34);
#8954=CIRCLE('',#24449,0.34);
#8955=CIRCLE('',#24453,0.3);
#8956=CIRCLE('',#24455,0.3);
#8957=CIRCLE('',#24457,0.3);
#8958=CIRCLE('',#24459,0.34);
#8959=CIRCLE('',#24461,0.34);
#8960=CIRCLE('',#24465,0.3);
#8961=CIRCLE('',#24467,0.3);
#8962=CIRCLE('',#24469,0.3);
#8963=CIRCLE('',#24471,0.34);
#8964=CIRCLE('',#24473,0.34);
#8965=CIRCLE('',#24477,0.3);
#8966=CIRCLE('',#24479,0.3);
#8967=CIRCLE('',#24481,0.3);
#8968=CIRCLE('',#24483,0.34);
#8969=CIRCLE('',#24485,0.34);
#8970=CIRCLE('',#24489,0.3);
#8971=CIRCLE('',#24491,0.3);
#8972=CIRCLE('',#24493,0.3);
#8973=CIRCLE('',#24495,0.34);
#8974=CIRCLE('',#24497,0.34);
#8975=CIRCLE('',#24501,0.34);
#8976=CIRCLE('',#24503,0.3);
#8977=CIRCLE('',#24505,0.3);
#8978=CIRCLE('',#24507,0.3);
#8979=CIRCLE('',#24510,0.34);
#8980=CIRCLE('',#24513,0.34);
#8981=CIRCLE('',#24517,1.5105713967741);
#8982=CIRCLE('',#24518,1.71158415478175);
#8983=CIRCLE('',#24519,1.71158415478175);
#8984=CIRCLE('',#24520,1.71158415478175);
#8985=CIRCLE('',#24521,1.71158415478175);
#8986=CIRCLE('',#24522,1.71158415478175);
#8987=CIRCLE('',#24523,1.71158415478175);
#8988=CIRCLE('',#24524,1.71158415478175);
#8989=CIRCLE('',#24525,1.71158415478175);
#8990=CIRCLE('',#24526,1.71158415478175);
#8991=CIRCLE('',#24527,1.71158415478175);
#8992=CIRCLE('',#24528,1.71158415478175);
#8993=CIRCLE('',#24529,1.71158415478175);
#8994=CIRCLE('',#24530,1.71158415478175);
#8995=CIRCLE('',#24531,1.71158415478175);
#8996=CIRCLE('',#24532,1.71158415478175);
#8997=CIRCLE('',#24533,1.71158415478175);
#8998=CIRCLE('',#24534,1.71158415478175);
#8999=CIRCLE('',#24535,1.71158415478175);
#9000=CIRCLE('',#24537,0.34);
#9001=CIRCLE('',#24541,0.34);
#9002=CIRCLE('',#24545,0.34);
#9003=CIRCLE('',#24549,0.34);
#9004=CIRCLE('',#24553,0.34);
#9005=CIRCLE('',#24557,0.34);
#9006=CIRCLE('',#24561,0.34);
#9007=CIRCLE('',#24565,0.34);
#9008=CIRCLE('',#24569,0.34);
#9009=CIRCLE('',#24573,0.34);
#9010=CIRCLE('',#24577,0.34);
#9011=CIRCLE('',#24581,0.34);
#9012=CIRCLE('',#24585,0.34);
#9013=CIRCLE('',#24589,0.34);
#9014=CIRCLE('',#24593,0.34);
#9015=CIRCLE('',#24598,0.34);
#9016=CIRCLE('',#24601,1.25);
#9017=CIRCLE('',#24602,1.31);
#9018=CIRCLE('',#24604,1.84);
#9019=CIRCLE('',#24606,1.9);
#9020=CIRCLE('',#24608,1.9);
#9021=CIRCLE('',#24611,1.6);
#9022=CIRCLE('',#24613,1.6);
#9023=CIRCLE('',#24615,1.31);
#9024=CIRCLE('',#24617,1.25);
#10616=VERTEX_POINT('',#47404);
#10617=VERTEX_POINT('',#47406);
#10618=VERTEX_POINT('',#47409);
#10619=VERTEX_POINT('',#47410);
#10620=VERTEX_POINT('',#47412);
#10621=VERTEX_POINT('',#47417);
#10622=VERTEX_POINT('',#47423);
#10623=VERTEX_POINT('',#47424);
#10624=VERTEX_POINT('',#47426);
#10625=VERTEX_POINT('',#47431);
#10626=VERTEX_POINT('',#47437);
#10627=VERTEX_POINT('',#47438);
#10628=VERTEX_POINT('',#47440);
#10629=VERTEX_POINT('',#47445);
#10630=VERTEX_POINT('',#47451);
#10631=VERTEX_POINT('',#47452);
#10632=VERTEX_POINT('',#47454);
#10633=VERTEX_POINT('',#47459);
#10634=VERTEX_POINT('',#47465);
#10635=VERTEX_POINT('',#47466);
#10636=VERTEX_POINT('',#47468);
#10637=VERTEX_POINT('',#47473);
#10638=VERTEX_POINT('',#47479);
#10639=VERTEX_POINT('',#47480);
#10640=VERTEX_POINT('',#47482);
#10641=VERTEX_POINT('',#47487);
#10642=VERTEX_POINT('',#47493);
#10643=VERTEX_POINT('',#47494);
#10644=VERTEX_POINT('',#47496);
#10645=VERTEX_POINT('',#47501);
#10646=VERTEX_POINT('',#47507);
#10647=VERTEX_POINT('',#47508);
#10648=VERTEX_POINT('',#47510);
#10649=VERTEX_POINT('',#47515);
#10650=VERTEX_POINT('',#47521);
#10651=VERTEX_POINT('',#47522);
#10652=VERTEX_POINT('',#47524);
#10653=VERTEX_POINT('',#47529);
#10654=VERTEX_POINT('',#47535);
#10655=VERTEX_POINT('',#47536);
#10656=VERTEX_POINT('',#47538);
#10657=VERTEX_POINT('',#47543);
#10658=VERTEX_POINT('',#47549);
#10659=VERTEX_POINT('',#47550);
#10660=VERTEX_POINT('',#47552);
#10661=VERTEX_POINT('',#47557);
#10662=VERTEX_POINT('',#47563);
#10663=VERTEX_POINT('',#47564);
#10664=VERTEX_POINT('',#47566);
#10665=VERTEX_POINT('',#47571);
#10666=VERTEX_POINT('',#47577);
#10667=VERTEX_POINT('',#47578);
#10668=VERTEX_POINT('',#47580);
#10669=VERTEX_POINT('',#47585);
#10670=VERTEX_POINT('',#47591);
#10671=VERTEX_POINT('',#47592);
#10672=VERTEX_POINT('',#47594);
#10673=VERTEX_POINT('',#47599);
#10674=VERTEX_POINT('',#47605);
#10675=VERTEX_POINT('',#47606);
#10676=VERTEX_POINT('',#47608);
#10677=VERTEX_POINT('',#47613);
#10678=VERTEX_POINT('',#47619);
#10679=VERTEX_POINT('',#47620);
#10680=VERTEX_POINT('',#47622);
#10681=VERTEX_POINT('',#47627);
#10682=VERTEX_POINT('',#47633);
#10683=VERTEX_POINT('',#47634);
#10684=VERTEX_POINT('',#47639);
#10685=VERTEX_POINT('',#47641);
#10686=VERTEX_POINT('',#47648);
#10687=VERTEX_POINT('',#47650);
#10688=VERTEX_POINT('',#47653);
#10689=VERTEX_POINT('',#47654);
#10690=VERTEX_POINT('',#47656);
#10691=VERTEX_POINT('',#47661);
#10692=VERTEX_POINT('',#47667);
#10693=VERTEX_POINT('',#47668);
#10694=VERTEX_POINT('',#47670);
#10695=VERTEX_POINT('',#47675);
#10696=VERTEX_POINT('',#47681);
#10697=VERTEX_POINT('',#47682);
#10698=VERTEX_POINT('',#47684);
#10699=VERTEX_POINT('',#47689);
#10700=VERTEX_POINT('',#47695);
#10701=VERTEX_POINT('',#47696);
#10702=VERTEX_POINT('',#47698);
#10703=VERTEX_POINT('',#47703);
#10704=VERTEX_POINT('',#47709);
#10705=VERTEX_POINT('',#47710);
#10706=VERTEX_POINT('',#47712);
#10707=VERTEX_POINT('',#47717);
#10708=VERTEX_POINT('',#47723);
#10709=VERTEX_POINT('',#47724);
#10710=VERTEX_POINT('',#47726);
#10711=VERTEX_POINT('',#47731);
#10712=VERTEX_POINT('',#47737);
#10713=VERTEX_POINT('',#47738);
#10714=VERTEX_POINT('',#47740);
#10715=VERTEX_POINT('',#47745);
#10716=VERTEX_POINT('',#47751);
#10717=VERTEX_POINT('',#47752);
#10718=VERTEX_POINT('',#47754);
#10719=VERTEX_POINT('',#47759);
#10720=VERTEX_POINT('',#47765);
#10721=VERTEX_POINT('',#47766);
#10722=VERTEX_POINT('',#47768);
#10723=VERTEX_POINT('',#47773);
#10724=VERTEX_POINT('',#47779);
#10725=VERTEX_POINT('',#47780);
#10726=VERTEX_POINT('',#47782);
#10727=VERTEX_POINT('',#47787);
#10728=VERTEX_POINT('',#47793);
#10729=VERTEX_POINT('',#47794);
#10730=VERTEX_POINT('',#47796);
#10731=VERTEX_POINT('',#47801);
#10732=VERTEX_POINT('',#47807);
#10733=VERTEX_POINT('',#47808);
#10734=VERTEX_POINT('',#47810);
#10735=VERTEX_POINT('',#47815);
#10736=VERTEX_POINT('',#47821);
#10737=VERTEX_POINT('',#47822);
#10738=VERTEX_POINT('',#47824);
#10739=VERTEX_POINT('',#47829);
#10740=VERTEX_POINT('',#47835);
#10741=VERTEX_POINT('',#47836);
#10742=VERTEX_POINT('',#47838);
#10743=VERTEX_POINT('',#47843);
#10744=VERTEX_POINT('',#47849);
#10745=VERTEX_POINT('',#47850);
#10746=VERTEX_POINT('',#47852);
#10747=VERTEX_POINT('',#47857);
#10748=VERTEX_POINT('',#47863);
#10749=VERTEX_POINT('',#47864);
#10750=VERTEX_POINT('',#47866);
#10751=VERTEX_POINT('',#47871);
#10752=VERTEX_POINT('',#47877);
#10753=VERTEX_POINT('',#47878);
#10754=VERTEX_POINT('',#47883);
#10755=VERTEX_POINT('',#47885);
#10756=VERTEX_POINT('',#47898);
#10757=VERTEX_POINT('',#47900);
#10758=VERTEX_POINT('',#47906);
#10759=VERTEX_POINT('',#47908);
#10760=VERTEX_POINT('',#47918);
#10761=VERTEX_POINT('',#47920);
#10762=VERTEX_POINT('',#47926);
#10763=VERTEX_POINT('',#47928);
#10764=VERTEX_POINT('',#47938);
#10765=VERTEX_POINT('',#47940);
#10766=VERTEX_POINT('',#47946);
#10767=VERTEX_POINT('',#47948);
#10768=VERTEX_POINT('',#47958);
#10769=VERTEX_POINT('',#47960);
#10770=VERTEX_POINT('',#47966);
#10771=VERTEX_POINT('',#47968);
#10772=VERTEX_POINT('',#47978);
#10773=VERTEX_POINT('',#47980);
#10774=VERTEX_POINT('',#47986);
#10775=VERTEX_POINT('',#47988);
#10776=VERTEX_POINT('',#47998);
#10777=VERTEX_POINT('',#48000);
#10778=VERTEX_POINT('',#48006);
#10779=VERTEX_POINT('',#48008);
#10780=VERTEX_POINT('',#48018);
#10781=VERTEX_POINT('',#48020);
#10782=VERTEX_POINT('',#48026);
#10783=VERTEX_POINT('',#48028);
#10784=VERTEX_POINT('',#48038);
#10785=VERTEX_POINT('',#48040);
#10786=VERTEX_POINT('',#48046);
#10787=VERTEX_POINT('',#48048);
#10788=VERTEX_POINT('',#48058);
#10789=VERTEX_POINT('',#48060);
#10790=VERTEX_POINT('',#48066);
#10791=VERTEX_POINT('',#48068);
#10792=VERTEX_POINT('',#48078);
#10793=VERTEX_POINT('',#48080);
#10794=VERTEX_POINT('',#48086);
#10795=VERTEX_POINT('',#48088);
#10796=VERTEX_POINT('',#48098);
#10797=VERTEX_POINT('',#48100);
#10798=VERTEX_POINT('',#48106);
#10799=VERTEX_POINT('',#48108);
#10800=VERTEX_POINT('',#48118);
#10801=VERTEX_POINT('',#48120);
#10802=VERTEX_POINT('',#48126);
#10803=VERTEX_POINT('',#48128);
#10804=VERTEX_POINT('',#48138);
#10805=VERTEX_POINT('',#48140);
#10806=VERTEX_POINT('',#48146);
#10807=VERTEX_POINT('',#48148);
#10808=VERTEX_POINT('',#48158);
#10809=VERTEX_POINT('',#48160);
#10810=VERTEX_POINT('',#48166);
#10811=VERTEX_POINT('',#48168);
#10812=VERTEX_POINT('',#48178);
#10813=VERTEX_POINT('',#48180);
#10814=VERTEX_POINT('',#48186);
#10815=VERTEX_POINT('',#48188);
#10816=VERTEX_POINT('',#48198);
#10817=VERTEX_POINT('',#48200);
#10818=VERTEX_POINT('',#48206);
#10819=VERTEX_POINT('',#48208);
#10820=VERTEX_POINT('',#48220);
#10821=VERTEX_POINT('',#48222);
#10822=VERTEX_POINT('',#48227);
#10823=VERTEX_POINT('',#48229);
#10824=VERTEX_POINT('',#48236);
#10825=VERTEX_POINT('',#48240);
#10826=VERTEX_POINT('',#48247);
#10827=VERTEX_POINT('',#48249);
#10828=VERTEX_POINT('',#48251);
#10829=VERTEX_POINT('',#48257);
#10830=VERTEX_POINT('',#48263);
#10831=VERTEX_POINT('',#48269);
#10832=VERTEX_POINT('',#48275);
#10833=VERTEX_POINT('',#48281);
#10834=VERTEX_POINT('',#48287);
#10835=VERTEX_POINT('',#48294);
#10836=VERTEX_POINT('',#48300);
#10837=VERTEX_POINT('',#48306);
#10838=VERTEX_POINT('',#48312);
#10839=VERTEX_POINT('',#48318);
#10840=VERTEX_POINT('',#48324);
#10841=VERTEX_POINT('',#48330);
#10842=VERTEX_POINT('',#48336);
#10843=VERTEX_POINT('',#48342);
#10844=VERTEX_POINT('',#48350);
#10845=VERTEX_POINT('',#48356);
#10846=VERTEX_POINT('',#48362);
#10847=VERTEX_POINT('',#48368);
#10848=VERTEX_POINT('',#48374);
#10849=VERTEX_POINT('',#48380);
#10850=VERTEX_POINT('',#48386);
#10851=VERTEX_POINT('',#48392);
#10852=VERTEX_POINT('',#48398);
#10853=VERTEX_POINT('',#48404);
#10854=VERTEX_POINT('',#48410);
#10855=VERTEX_POINT('',#48416);
#10856=VERTEX_POINT('',#48422);
#10857=VERTEX_POINT('',#48428);
#10858=VERTEX_POINT('',#48434);
#10859=VERTEX_POINT('',#48440);
#10860=VERTEX_POINT('',#48446);
#10861=VERTEX_POINT('',#48448);
#10862=VERTEX_POINT('',#48452);
#10863=VERTEX_POINT('',#48455);
#10864=VERTEX_POINT('',#48459);
#10865=VERTEX_POINT('',#48464);
#10866=VERTEX_POINT('',#48467);
#10867=VERTEX_POINT('',#48471);
#10868=VERTEX_POINT('',#48474);
#13538=EDGE_CURVE('',#10616,#10616,#8891,.T.);
#13539=EDGE_CURVE('',#10616,#10617,#6510,.T.);
#13540=EDGE_CURVE('',#10617,#10617,#8892,.T.);
#13541=EDGE_CURVE('',#10618,#10619,#191,.T.);
#13542=EDGE_CURVE('',#10618,#10620,#1175,.T.);
#13543=EDGE_CURVE('',#10621,#10620,#192,.T.);
#13544=EDGE_CURVE('',#10621,#10619,#1176,.T.);
#13545=EDGE_CURVE('',#10622,#10623,#193,.T.);
#13546=EDGE_CURVE('',#10622,#10624,#1177,.T.);
#13547=EDGE_CURVE('',#10625,#10624,#194,.T.);
#13548=EDGE_CURVE('',#10625,#10623,#1178,.T.);
#13549=EDGE_CURVE('',#10626,#10627,#195,.T.);
#13550=EDGE_CURVE('',#10626,#10628,#1179,.T.);
#13551=EDGE_CURVE('',#10629,#10628,#196,.T.);
#13552=EDGE_CURVE('',#10629,#10627,#1180,.T.);
#13553=EDGE_CURVE('',#10630,#10631,#197,.T.);
#13554=EDGE_CURVE('',#10630,#10632,#1181,.T.);
#13555=EDGE_CURVE('',#10633,#10632,#198,.T.);
#13556=EDGE_CURVE('',#10633,#10631,#1182,.T.);
#13557=EDGE_CURVE('',#10634,#10635,#199,.T.);
#13558=EDGE_CURVE('',#10634,#10636,#1183,.T.);
#13559=EDGE_CURVE('',#10637,#10636,#200,.T.);
#13560=EDGE_CURVE('',#10637,#10635,#1184,.T.);
#13561=EDGE_CURVE('',#10638,#10639,#201,.T.);
#13562=EDGE_CURVE('',#10638,#10640,#1185,.T.);
#13563=EDGE_CURVE('',#10641,#10640,#202,.T.);
#13564=EDGE_CURVE('',#10641,#10639,#1186,.T.);
#13565=EDGE_CURVE('',#10642,#10643,#203,.T.);
#13566=EDGE_CURVE('',#10642,#10644,#1187,.T.);
#13567=EDGE_CURVE('',#10645,#10644,#204,.T.);
#13568=EDGE_CURVE('',#10645,#10643,#1188,.T.);
#13569=EDGE_CURVE('',#10646,#10647,#205,.T.);
#13570=EDGE_CURVE('',#10646,#10648,#1189,.T.);
#13571=EDGE_CURVE('',#10649,#10648,#206,.T.);
#13572=EDGE_CURVE('',#10649,#10647,#1190,.T.);
#13573=EDGE_CURVE('',#10650,#10651,#207,.T.);
#13574=EDGE_CURVE('',#10650,#10652,#1191,.T.);
#13575=EDGE_CURVE('',#10653,#10652,#208,.T.);
#13576=EDGE_CURVE('',#10653,#10651,#1192,.T.);
#13577=EDGE_CURVE('',#10654,#10655,#209,.T.);
#13578=EDGE_CURVE('',#10654,#10656,#1193,.T.);
#13579=EDGE_CURVE('',#10657,#10656,#210,.T.);
#13580=EDGE_CURVE('',#10657,#10655,#1194,.T.);
#13581=EDGE_CURVE('',#10658,#10659,#211,.T.);
#13582=EDGE_CURVE('',#10658,#10660,#1195,.T.);
#13583=EDGE_CURVE('',#10661,#10660,#212,.T.);
#13584=EDGE_CURVE('',#10661,#10659,#1196,.T.);
#13585=EDGE_CURVE('',#10662,#10663,#213,.T.);
#13586=EDGE_CURVE('',#10662,#10664,#1197,.T.);
#13587=EDGE_CURVE('',#10665,#10664,#214,.T.);
#13588=EDGE_CURVE('',#10665,#10663,#1198,.T.);
#13589=EDGE_CURVE('',#10666,#10667,#215,.T.);
#13590=EDGE_CURVE('',#10666,#10668,#1199,.T.);
#13591=EDGE_CURVE('',#10669,#10668,#216,.T.);
#13592=EDGE_CURVE('',#10669,#10667,#1200,.T.);
#13593=EDGE_CURVE('',#10670,#10671,#217,.T.);
#13594=EDGE_CURVE('',#10670,#10672,#1201,.T.);
#13595=EDGE_CURVE('',#10673,#10672,#218,.T.);
#13596=EDGE_CURVE('',#10673,#10671,#1202,.T.);
#13597=EDGE_CURVE('',#10674,#10675,#219,.T.);
#13598=EDGE_CURVE('',#10674,#10676,#1203,.T.);
#13599=EDGE_CURVE('',#10677,#10676,#220,.T.);
#13600=EDGE_CURVE('',#10677,#10675,#1204,.T.);
#13601=EDGE_CURVE('',#10678,#10679,#221,.T.);
#13602=EDGE_CURVE('',#10678,#10680,#1205,.T.);
#13603=EDGE_CURVE('',#10681,#10680,#222,.T.);
#13604=EDGE_CURVE('',#10681,#10679,#1206,.T.);
#13605=EDGE_CURVE('',#10682,#10683,#1207,.T.);
#13606=EDGE_CURVE('',#10684,#10683,#223,.T.);
#13607=EDGE_CURVE('',#10684,#10685,#1208,.T.);
#13608=EDGE_CURVE('',#10682,#10685,#224,.T.);
#13609=EDGE_CURVE('',#10686,#10686,#8893,.T.);
#13610=EDGE_CURVE('',#10686,#10687,#6511,.T.);
#13611=EDGE_CURVE('',#10687,#10687,#8894,.T.);
#13612=EDGE_CURVE('',#10688,#10689,#225,.T.);
#13613=EDGE_CURVE('',#10688,#10690,#1209,.T.);
#13614=EDGE_CURVE('',#10691,#10690,#226,.T.);
#13615=EDGE_CURVE('',#10691,#10689,#1210,.T.);
#13616=EDGE_CURVE('',#10692,#10693,#227,.T.);
#13617=EDGE_CURVE('',#10692,#10694,#1211,.T.);
#13618=EDGE_CURVE('',#10695,#10694,#228,.T.);
#13619=EDGE_CURVE('',#10695,#10693,#1212,.T.);
#13620=EDGE_CURVE('',#10696,#10697,#229,.T.);
#13621=EDGE_CURVE('',#10696,#10698,#1213,.T.);
#13622=EDGE_CURVE('',#10699,#10698,#230,.T.);
#13623=EDGE_CURVE('',#10699,#10697,#1214,.T.);
#13624=EDGE_CURVE('',#10700,#10701,#231,.T.);
#13625=EDGE_CURVE('',#10700,#10702,#1215,.T.);
#13626=EDGE_CURVE('',#10703,#10702,#232,.T.);
#13627=EDGE_CURVE('',#10703,#10701,#1216,.T.);
#13628=EDGE_CURVE('',#10704,#10705,#233,.T.);
#13629=EDGE_CURVE('',#10704,#10706,#1217,.T.);
#13630=EDGE_CURVE('',#10707,#10706,#234,.T.);
#13631=EDGE_CURVE('',#10707,#10705,#1218,.T.);
#13632=EDGE_CURVE('',#10708,#10709,#235,.T.);
#13633=EDGE_CURVE('',#10708,#10710,#1219,.T.);
#13634=EDGE_CURVE('',#10711,#10710,#236,.T.);
#13635=EDGE_CURVE('',#10711,#10709,#1220,.T.);
#13636=EDGE_CURVE('',#10712,#10713,#237,.T.);
#13637=EDGE_CURVE('',#10712,#10714,#1221,.T.);
#13638=EDGE_CURVE('',#10715,#10714,#238,.T.);
#13639=EDGE_CURVE('',#10715,#10713,#1222,.T.);
#13640=EDGE_CURVE('',#10716,#10717,#239,.T.);
#13641=EDGE_CURVE('',#10716,#10718,#1223,.T.);
#13642=EDGE_CURVE('',#10719,#10718,#240,.T.);
#13643=EDGE_CURVE('',#10719,#10717,#1224,.T.);
#13644=EDGE_CURVE('',#10720,#10721,#241,.T.);
#13645=EDGE_CURVE('',#10720,#10722,#1225,.T.);
#13646=EDGE_CURVE('',#10723,#10722,#242,.T.);
#13647=EDGE_CURVE('',#10723,#10721,#1226,.T.);
#13648=EDGE_CURVE('',#10724,#10725,#243,.T.);
#13649=EDGE_CURVE('',#10724,#10726,#1227,.T.);
#13650=EDGE_CURVE('',#10727,#10726,#244,.T.);
#13651=EDGE_CURVE('',#10727,#10725,#1228,.T.);
#13652=EDGE_CURVE('',#10728,#10729,#245,.T.);
#13653=EDGE_CURVE('',#10728,#10730,#1229,.T.);
#13654=EDGE_CURVE('',#10731,#10730,#246,.T.);
#13655=EDGE_CURVE('',#10731,#10729,#1230,.T.);
#13656=EDGE_CURVE('',#10732,#10733,#247,.T.);
#13657=EDGE_CURVE('',#10732,#10734,#1231,.T.);
#13658=EDGE_CURVE('',#10735,#10734,#248,.T.);
#13659=EDGE_CURVE('',#10735,#10733,#1232,.T.);
#13660=EDGE_CURVE('',#10736,#10737,#249,.T.);
#13661=EDGE_CURVE('',#10736,#10738,#1233,.T.);
#13662=EDGE_CURVE('',#10739,#10738,#250,.T.);
#13663=EDGE_CURVE('',#10739,#10737,#1234,.T.);
#13664=EDGE_CURVE('',#10740,#10741,#251,.T.);
#13665=EDGE_CURVE('',#10740,#10742,#1235,.T.);
#13666=EDGE_CURVE('',#10743,#10742,#252,.T.);
#13667=EDGE_CURVE('',#10743,#10741,#1236,.T.);
#13668=EDGE_CURVE('',#10744,#10745,#253,.T.);
#13669=EDGE_CURVE('',#10744,#10746,#1237,.T.);
#13670=EDGE_CURVE('',#10747,#10746,#254,.T.);
#13671=EDGE_CURVE('',#10747,#10745,#1238,.T.);
#13672=EDGE_CURVE('',#10748,#10749,#255,.T.);
#13673=EDGE_CURVE('',#10748,#10750,#1239,.T.);
#13674=EDGE_CURVE('',#10751,#10750,#256,.T.);
#13675=EDGE_CURVE('',#10751,#10749,#1240,.T.);
#13676=EDGE_CURVE('',#10752,#10753,#1241,.T.);
#13677=EDGE_CURVE('',#10754,#10753,#257,.T.);
#13678=EDGE_CURVE('',#10754,#10755,#1242,.T.);
#13679=EDGE_CURVE('',#10752,#10755,#258,.T.);
#13680=EDGE_CURVE('',#10687,#10617,#6512,.T.);
#13681=EDGE_CURVE('',#10686,#10616,#6513,.T.);
#13682=EDGE_CURVE('',#10690,#10691,#8895,.T.);
#13683=EDGE_CURVE('',#10620,#10756,#8896,.T.);
#13684=EDGE_CURVE('',#10757,#10756,#259,.T.);
#13685=EDGE_CURVE('',#10757,#10621,#8897,.T.);
#13686=EDGE_CURVE('',#10688,#10689,#8898,.T.);
#13687=EDGE_CURVE('',#10618,#10758,#8899,.T.);
#13688=EDGE_CURVE('',#10759,#10758,#260,.T.);
#13689=EDGE_CURVE('',#10756,#10759,#1243,.T.);
#13690=EDGE_CURVE('',#10694,#10695,#8900,.T.);
#13691=EDGE_CURVE('',#10624,#10760,#8901,.T.);
#13692=EDGE_CURVE('',#10761,#10760,#261,.T.);
#13693=EDGE_CURVE('',#10761,#10625,#8902,.T.);
#13694=EDGE_CURVE('',#10692,#10693,#8903,.T.);
#13695=EDGE_CURVE('',#10622,#10762,#8904,.T.);
#13696=EDGE_CURVE('',#10763,#10762,#262,.T.);
#13697=EDGE_CURVE('',#10760,#10763,#1244,.T.);
#13698=EDGE_CURVE('',#10698,#10699,#8905,.T.);
#13699=EDGE_CURVE('',#10628,#10764,#8906,.T.);
#13700=EDGE_CURVE('',#10765,#10764,#263,.T.);
#13701=EDGE_CURVE('',#10765,#10629,#8907,.T.);
#13702=EDGE_CURVE('',#10696,#10697,#8908,.T.);
#13703=EDGE_CURVE('',#10626,#10766,#8909,.T.);
#13704=EDGE_CURVE('',#10767,#10766,#264,.T.);
#13705=EDGE_CURVE('',#10764,#10767,#1245,.T.);
#13706=EDGE_CURVE('',#10702,#10703,#8910,.T.);
#13707=EDGE_CURVE('',#10632,#10768,#8911,.T.);
#13708=EDGE_CURVE('',#10769,#10768,#265,.T.);
#13709=EDGE_CURVE('',#10769,#10633,#8912,.T.);
#13710=EDGE_CURVE('',#10700,#10701,#8913,.T.);
#13711=EDGE_CURVE('',#10630,#10770,#8914,.T.);
#13712=EDGE_CURVE('',#10771,#10770,#266,.T.);
#13713=EDGE_CURVE('',#10768,#10771,#1246,.T.);
#13714=EDGE_CURVE('',#10706,#10707,#8915,.T.);
#13715=EDGE_CURVE('',#10636,#10772,#8916,.T.);
#13716=EDGE_CURVE('',#10773,#10772,#267,.T.);
#13717=EDGE_CURVE('',#10773,#10637,#8917,.T.);
#13718=EDGE_CURVE('',#10704,#10705,#8918,.T.);
#13719=EDGE_CURVE('',#10634,#10774,#8919,.T.);
#13720=EDGE_CURVE('',#10775,#10774,#268,.T.);
#13721=EDGE_CURVE('',#10772,#10775,#1247,.T.);
#13722=EDGE_CURVE('',#10710,#10711,#8920,.T.);
#13723=EDGE_CURVE('',#10640,#10776,#8921,.T.);
#13724=EDGE_CURVE('',#10777,#10776,#269,.T.);
#13725=EDGE_CURVE('',#10777,#10641,#8922,.T.);
#13726=EDGE_CURVE('',#10708,#10709,#8923,.T.);
#13727=EDGE_CURVE('',#10638,#10778,#8924,.T.);
#13728=EDGE_CURVE('',#10779,#10778,#270,.T.);
#13729=EDGE_CURVE('',#10776,#10779,#1248,.T.);
#13730=EDGE_CURVE('',#10714,#10715,#8925,.T.);
#13731=EDGE_CURVE('',#10644,#10780,#8926,.T.);
#13732=EDGE_CURVE('',#10781,#10780,#271,.T.);
#13733=EDGE_CURVE('',#10781,#10645,#8927,.T.);
#13734=EDGE_CURVE('',#10712,#10713,#8928,.T.);
#13735=EDGE_CURVE('',#10642,#10782,#8929,.T.);
#13736=EDGE_CURVE('',#10783,#10782,#272,.T.);
#13737=EDGE_CURVE('',#10780,#10783,#1249,.T.);
#13738=EDGE_CURVE('',#10718,#10719,#8930,.T.);
#13739=EDGE_CURVE('',#10648,#10784,#8931,.T.);
#13740=EDGE_CURVE('',#10785,#10784,#273,.T.);
#13741=EDGE_CURVE('',#10785,#10649,#8932,.T.);
#13742=EDGE_CURVE('',#10716,#10717,#8933,.T.);
#13743=EDGE_CURVE('',#10646,#10786,#8934,.T.);
#13744=EDGE_CURVE('',#10787,#10786,#274,.T.);
#13745=EDGE_CURVE('',#10784,#10787,#1250,.T.);
#13746=EDGE_CURVE('',#10722,#10723,#8935,.T.);
#13747=EDGE_CURVE('',#10652,#10788,#8936,.T.);
#13748=EDGE_CURVE('',#10789,#10788,#275,.T.);
#13749=EDGE_CURVE('',#10789,#10653,#8937,.T.);
#13750=EDGE_CURVE('',#10720,#10721,#8938,.T.);
#13751=EDGE_CURVE('',#10650,#10790,#8939,.T.);
#13752=EDGE_CURVE('',#10791,#10790,#276,.T.);
#13753=EDGE_CURVE('',#10788,#10791,#1251,.T.);
#13754=EDGE_CURVE('',#10726,#10727,#8940,.T.);
#13755=EDGE_CURVE('',#10656,#10792,#8941,.T.);
#13756=EDGE_CURVE('',#10793,#10792,#277,.T.);
#13757=EDGE_CURVE('',#10793,#10657,#8942,.T.);
#13758=EDGE_CURVE('',#10724,#10725,#8943,.T.);
#13759=EDGE_CURVE('',#10654,#10794,#8944,.T.);
#13760=EDGE_CURVE('',#10795,#10794,#278,.T.);
#13761=EDGE_CURVE('',#10792,#10795,#1252,.T.);
#13762=EDGE_CURVE('',#10730,#10731,#8945,.T.);
#13763=EDGE_CURVE('',#10660,#10796,#8946,.T.);
#13764=EDGE_CURVE('',#10797,#10796,#279,.T.);
#13765=EDGE_CURVE('',#10797,#10661,#8947,.T.);
#13766=EDGE_CURVE('',#10728,#10729,#8948,.T.);
#13767=EDGE_CURVE('',#10658,#10798,#8949,.T.);
#13768=EDGE_CURVE('',#10799,#10798,#280,.T.);
#13769=EDGE_CURVE('',#10796,#10799,#1253,.T.);
#13770=EDGE_CURVE('',#10734,#10735,#8950,.T.);
#13771=EDGE_CURVE('',#10664,#10800,#8951,.T.);
#13772=EDGE_CURVE('',#10801,#10800,#281,.T.);
#13773=EDGE_CURVE('',#10801,#10665,#8952,.T.);
#13774=EDGE_CURVE('',#10732,#10733,#8953,.T.);
#13775=EDGE_CURVE('',#10662,#10802,#8954,.T.);
#13776=EDGE_CURVE('',#10803,#10802,#282,.T.);
#13777=EDGE_CURVE('',#10800,#10803,#1254,.T.);
#13778=EDGE_CURVE('',#10738,#10739,#8955,.T.);
#13779=EDGE_CURVE('',#10668,#10804,#8956,.T.);
#13780=EDGE_CURVE('',#10805,#10804,#283,.T.);
#13781=EDGE_CURVE('',#10805,#10669,#8957,.T.);
#13782=EDGE_CURVE('',#10736,#10737,#8958,.T.);
#13783=EDGE_CURVE('',#10666,#10806,#8959,.T.);
#13784=EDGE_CURVE('',#10807,#10806,#284,.T.);
#13785=EDGE_CURVE('',#10804,#10807,#1255,.T.);
#13786=EDGE_CURVE('',#10742,#10743,#8960,.T.);
#13787=EDGE_CURVE('',#10672,#10808,#8961,.T.);
#13788=EDGE_CURVE('',#10809,#10808,#285,.T.);
#13789=EDGE_CURVE('',#10809,#10673,#8962,.T.);
#13790=EDGE_CURVE('',#10740,#10741,#8963,.T.);
#13791=EDGE_CURVE('',#10670,#10810,#8964,.T.);
#13792=EDGE_CURVE('',#10811,#10810,#286,.T.);
#13793=EDGE_CURVE('',#10808,#10811,#1256,.T.);
#13794=EDGE_CURVE('',#10746,#10747,#8965,.T.);
#13795=EDGE_CURVE('',#10676,#10812,#8966,.T.);
#13796=EDGE_CURVE('',#10813,#10812,#287,.T.);
#13797=EDGE_CURVE('',#10813,#10677,#8967,.T.);
#13798=EDGE_CURVE('',#10744,#10745,#8968,.T.);
#13799=EDGE_CURVE('',#10674,#10814,#8969,.T.);
#13800=EDGE_CURVE('',#10815,#10814,#288,.T.);
#13801=EDGE_CURVE('',#10812,#10815,#1257,.T.);
#13802=EDGE_CURVE('',#10750,#10751,#8970,.T.);
#13803=EDGE_CURVE('',#10680,#10816,#8971,.T.);
#13804=EDGE_CURVE('',#10817,#10816,#289,.T.);
#13805=EDGE_CURVE('',#10817,#10681,#8972,.T.);
#13806=EDGE_CURVE('',#10748,#10749,#8973,.T.);
#13807=EDGE_CURVE('',#10678,#10818,#8974,.T.);
#13808=EDGE_CURVE('',#10819,#10818,#290,.T.);
#13809=EDGE_CURVE('',#10816,#10819,#1258,.T.);
#13810=EDGE_CURVE('',#10754,#10753,#8975,.T.);
#13811=EDGE_CURVE('',#10755,#10752,#8976,.T.);
#13812=EDGE_CURVE('',#10683,#10820,#8977,.T.);
#13813=EDGE_CURVE('',#10821,#10820,#291,.T.);
#13814=EDGE_CURVE('',#10821,#10684,#8978,.T.);
#13815=EDGE_CURVE('',#10682,#10822,#8979,.T.);
#13816=EDGE_CURVE('',#10823,#10822,#292,.T.);
#13817=EDGE_CURVE('',#10820,#10823,#1259,.T.);
#13818=EDGE_CURVE('',#10824,#10619,#8980,.T.);
#13819=EDGE_CURVE('',#10758,#10824,#6514,.T.);
#13820=EDGE_CURVE('',#10825,#10757,#1260,.T.);
#13821=EDGE_CURVE('',#10824,#10825,#293,.T.);
#13822=EDGE_CURVE('',#10826,#10826,#8981,.T.);
#13823=EDGE_CURVE('',#10826,#10827,#6515,.T.);
#13824=EDGE_CURVE('',#10827,#10828,#8982,.T.);
#13825=EDGE_CURVE('',#10828,#10785,#1261,.T.);
#13826=EDGE_CURVE('',#10787,#10829,#8983,.T.);
#13827=EDGE_CURVE('',#10829,#10781,#1262,.T.);
#13828=EDGE_CURVE('',#10783,#10830,#8984,.T.);
#13829=EDGE_CURVE('',#10830,#10777,#1263,.T.);
#13830=EDGE_CURVE('',#10779,#10831,#8985,.T.);
#13831=EDGE_CURVE('',#10831,#10773,#1264,.T.);
#13832=EDGE_CURVE('',#10775,#10832,#8986,.T.);
#13833=EDGE_CURVE('',#10832,#10769,#1265,.T.);
#13834=EDGE_CURVE('',#10771,#10833,#8987,.T.);
#13835=EDGE_CURVE('',#10833,#10765,#1266,.T.);
#13836=EDGE_CURVE('',#10767,#10834,#8988,.T.);
#13837=EDGE_CURVE('',#10834,#10761,#1267,.T.);
#13838=EDGE_CURVE('',#10763,#10825,#8989,.T.);
#13839=EDGE_CURVE('',#10759,#10835,#8990,.T.);
#13840=EDGE_CURVE('',#10835,#10821,#1268,.T.);
#13841=EDGE_CURVE('',#10823,#10836,#8991,.T.);
#13842=EDGE_CURVE('',#10836,#10817,#1269,.T.);
#13843=EDGE_CURVE('',#10819,#10837,#8992,.T.);
#13844=EDGE_CURVE('',#10837,#10813,#1270,.T.);
#13845=EDGE_CURVE('',#10815,#10838,#8993,.T.);
#13846=EDGE_CURVE('',#10838,#10809,#1271,.T.);
#13847=EDGE_CURVE('',#10811,#10839,#8994,.T.);
#13848=EDGE_CURVE('',#10839,#10805,#1272,.T.);
#13849=EDGE_CURVE('',#10807,#10840,#8995,.T.);
#13850=EDGE_CURVE('',#10840,#10801,#1273,.T.);
#13851=EDGE_CURVE('',#10803,#10841,#8996,.T.);
#13852=EDGE_CURVE('',#10841,#10797,#1274,.T.);
#13853=EDGE_CURVE('',#10799,#10842,#8997,.T.);
#13854=EDGE_CURVE('',#10842,#10793,#1275,.T.);
#13855=EDGE_CURVE('',#10795,#10843,#8998,.T.);
#13856=EDGE_CURVE('',#10843,#10789,#1276,.T.);
#13857=EDGE_CURVE('',#10791,#10827,#8999,.T.);
#13858=EDGE_CURVE('',#10844,#10623,#9000,.T.);
#13859=EDGE_CURVE('',#10762,#10844,#6516,.T.);
#13860=EDGE_CURVE('',#10844,#10834,#294,.T.);
#13861=EDGE_CURVE('',#10845,#10627,#9001,.T.);
#13862=EDGE_CURVE('',#10766,#10845,#6517,.T.);
#13863=EDGE_CURVE('',#10845,#10833,#295,.T.);
#13864=EDGE_CURVE('',#10846,#10631,#9002,.T.);
#13865=EDGE_CURVE('',#10770,#10846,#6518,.T.);
#13866=EDGE_CURVE('',#10846,#10832,#296,.T.);
#13867=EDGE_CURVE('',#10847,#10635,#9003,.T.);
#13868=EDGE_CURVE('',#10774,#10847,#6519,.T.);
#13869=EDGE_CURVE('',#10847,#10831,#297,.T.);
#13870=EDGE_CURVE('',#10848,#10639,#9004,.T.);
#13871=EDGE_CURVE('',#10778,#10848,#6520,.T.);
#13872=EDGE_CURVE('',#10848,#10830,#298,.T.);
#13873=EDGE_CURVE('',#10849,#10643,#9005,.T.);
#13874=EDGE_CURVE('',#10782,#10849,#6521,.T.);
#13875=EDGE_CURVE('',#10849,#10829,#299,.T.);
#13876=EDGE_CURVE('',#10850,#10647,#9006,.T.);
#13877=EDGE_CURVE('',#10786,#10850,#6522,.T.);
#13878=EDGE_CURVE('',#10850,#10828,#300,.T.);
#13879=EDGE_CURVE('',#10851,#10651,#9007,.T.);
#13880=EDGE_CURVE('',#10790,#10851,#6523,.T.);
#13881=EDGE_CURVE('',#10851,#10843,#301,.T.);
#13882=EDGE_CURVE('',#10852,#10655,#9008,.T.);
#13883=EDGE_CURVE('',#10794,#10852,#6524,.T.);
#13884=EDGE_CURVE('',#10852,#10842,#302,.T.);
#13885=EDGE_CURVE('',#10853,#10659,#9009,.T.);
#13886=EDGE_CURVE('',#10798,#10853,#6525,.T.);
#13887=EDGE_CURVE('',#10853,#10841,#303,.T.);
#13888=EDGE_CURVE('',#10854,#10663,#9010,.T.);
#13889=EDGE_CURVE('',#10802,#10854,#6526,.T.);
#13890=EDGE_CURVE('',#10854,#10840,#304,.T.);
#13891=EDGE_CURVE('',#10855,#10667,#9011,.T.);
#13892=EDGE_CURVE('',#10806,#10855,#6527,.T.);
#13893=EDGE_CURVE('',#10855,#10839,#305,.T.);
#13894=EDGE_CURVE('',#10856,#10671,#9012,.T.);
#13895=EDGE_CURVE('',#10810,#10856,#6528,.T.);
#13896=EDGE_CURVE('',#10856,#10838,#306,.T.);
#13897=EDGE_CURVE('',#10857,#10675,#9013,.T.);
#13898=EDGE_CURVE('',#10814,#10857,#6529,.T.);
#13899=EDGE_CURVE('',#10857,#10837,#307,.T.);
#13900=EDGE_CURVE('',#10858,#10679,#9014,.T.);
#13901=EDGE_CURVE('',#10818,#10858,#6530,.T.);
#13902=EDGE_CURVE('',#10858,#10836,#308,.T.);
#13903=EDGE_CURVE('',#10859,#10835,#309,.T.);
#13904=EDGE_CURVE('',#10859,#10685,#9015,.T.);
#13905=EDGE_CURVE('',#10822,#10859,#6531,.T.);
#13906=EDGE_CURVE('',#10860,#10860,#9016,.T.);
#13907=EDGE_CURVE('',#10860,#10861,#6532,.T.);
#13908=EDGE_CURVE('',#10861,#10861,#9017,.T.);
#13909=EDGE_CURVE('',#10862,#10862,#9018,.T.);
#13910=EDGE_CURVE('',#10863,#10863,#9019,.T.);
#13911=EDGE_CURVE('',#10863,#10862,#6533,.T.);
#13912=EDGE_CURVE('',#10864,#10864,#9020,.T.);
#13913=EDGE_CURVE('',#10864,#10863,#6534,.T.);
#13914=EDGE_CURVE('',#10865,#10865,#9021,.T.);
#13915=EDGE_CURVE('',#10866,#10866,#9022,.T.);
#13916=EDGE_CURVE('',#10866,#10865,#6535,.T.);
#13917=EDGE_CURVE('',#10867,#10867,#9023,.T.);
#13918=EDGE_CURVE('',#10867,#10868,#6536,.T.);
#13919=EDGE_CURVE('',#10868,#10868,#9024,.T.);
#13920=EDGE_CURVE('',#10868,#10860,#6537,.T.);
#19068=ORIENTED_EDGE('',*,*,#13538,.T.);
#19069=ORIENTED_EDGE('',*,*,#13539,.T.);
#19070=ORIENTED_EDGE('',*,*,#13540,.F.);
#19071=ORIENTED_EDGE('',*,*,#13539,.F.);
#19072=ORIENTED_EDGE('',*,*,#13541,.F.);
#19073=ORIENTED_EDGE('',*,*,#13542,.T.);
#19074=ORIENTED_EDGE('',*,*,#13543,.F.);
#19075=ORIENTED_EDGE('',*,*,#13544,.T.);
#19076=ORIENTED_EDGE('',*,*,#13545,.F.);
#19077=ORIENTED_EDGE('',*,*,#13546,.T.);
#19078=ORIENTED_EDGE('',*,*,#13547,.F.);
#19079=ORIENTED_EDGE('',*,*,#13548,.T.);
#19080=ORIENTED_EDGE('',*,*,#13549,.F.);
#19081=ORIENTED_EDGE('',*,*,#13550,.T.);
#19082=ORIENTED_EDGE('',*,*,#13551,.F.);
#19083=ORIENTED_EDGE('',*,*,#13552,.T.);
#19084=ORIENTED_EDGE('',*,*,#13553,.F.);
#19085=ORIENTED_EDGE('',*,*,#13554,.T.);
#19086=ORIENTED_EDGE('',*,*,#13555,.F.);
#19087=ORIENTED_EDGE('',*,*,#13556,.T.);
#19088=ORIENTED_EDGE('',*,*,#13557,.F.);
#19089=ORIENTED_EDGE('',*,*,#13558,.T.);
#19090=ORIENTED_EDGE('',*,*,#13559,.F.);
#19091=ORIENTED_EDGE('',*,*,#13560,.T.);
#19092=ORIENTED_EDGE('',*,*,#13561,.F.);
#19093=ORIENTED_EDGE('',*,*,#13562,.T.);
#19094=ORIENTED_EDGE('',*,*,#13563,.F.);
#19095=ORIENTED_EDGE('',*,*,#13564,.T.);
#19096=ORIENTED_EDGE('',*,*,#13565,.F.);
#19097=ORIENTED_EDGE('',*,*,#13566,.T.);
#19098=ORIENTED_EDGE('',*,*,#13567,.F.);
#19099=ORIENTED_EDGE('',*,*,#13568,.T.);
#19100=ORIENTED_EDGE('',*,*,#13569,.F.);
#19101=ORIENTED_EDGE('',*,*,#13570,.T.);
#19102=ORIENTED_EDGE('',*,*,#13571,.F.);
#19103=ORIENTED_EDGE('',*,*,#13572,.T.);
#19104=ORIENTED_EDGE('',*,*,#13573,.F.);
#19105=ORIENTED_EDGE('',*,*,#13574,.T.);
#19106=ORIENTED_EDGE('',*,*,#13575,.F.);
#19107=ORIENTED_EDGE('',*,*,#13576,.T.);
#19108=ORIENTED_EDGE('',*,*,#13577,.F.);
#19109=ORIENTED_EDGE('',*,*,#13578,.T.);
#19110=ORIENTED_EDGE('',*,*,#13579,.F.);
#19111=ORIENTED_EDGE('',*,*,#13580,.T.);
#19112=ORIENTED_EDGE('',*,*,#13581,.F.);
#19113=ORIENTED_EDGE('',*,*,#13582,.T.);
#19114=ORIENTED_EDGE('',*,*,#13583,.F.);
#19115=ORIENTED_EDGE('',*,*,#13584,.T.);
#19116=ORIENTED_EDGE('',*,*,#13585,.F.);
#19117=ORIENTED_EDGE('',*,*,#13586,.T.);
#19118=ORIENTED_EDGE('',*,*,#13587,.F.);
#19119=ORIENTED_EDGE('',*,*,#13588,.T.);
#19120=ORIENTED_EDGE('',*,*,#13589,.F.);
#19121=ORIENTED_EDGE('',*,*,#13590,.T.);
#19122=ORIENTED_EDGE('',*,*,#13591,.F.);
#19123=ORIENTED_EDGE('',*,*,#13592,.T.);
#19124=ORIENTED_EDGE('',*,*,#13593,.F.);
#19125=ORIENTED_EDGE('',*,*,#13594,.T.);
#19126=ORIENTED_EDGE('',*,*,#13595,.F.);
#19127=ORIENTED_EDGE('',*,*,#13596,.T.);
#19128=ORIENTED_EDGE('',*,*,#13597,.F.);
#19129=ORIENTED_EDGE('',*,*,#13598,.T.);
#19130=ORIENTED_EDGE('',*,*,#13599,.F.);
#19131=ORIENTED_EDGE('',*,*,#13600,.T.);
#19132=ORIENTED_EDGE('',*,*,#13601,.F.);
#19133=ORIENTED_EDGE('',*,*,#13602,.T.);
#19134=ORIENTED_EDGE('',*,*,#13603,.F.);
#19135=ORIENTED_EDGE('',*,*,#13604,.T.);
#19136=ORIENTED_EDGE('',*,*,#13605,.T.);
#19137=ORIENTED_EDGE('',*,*,#13606,.F.);
#19138=ORIENTED_EDGE('',*,*,#13607,.T.);
#19139=ORIENTED_EDGE('',*,*,#13608,.F.);
#19140=ORIENTED_EDGE('',*,*,#13609,.F.);
#19141=ORIENTED_EDGE('',*,*,#13610,.T.);
#19142=ORIENTED_EDGE('',*,*,#13611,.T.);
#19143=ORIENTED_EDGE('',*,*,#13610,.F.);
#19144=ORIENTED_EDGE('',*,*,#13612,.F.);
#19145=ORIENTED_EDGE('',*,*,#13613,.T.);
#19146=ORIENTED_EDGE('',*,*,#13614,.F.);
#19147=ORIENTED_EDGE('',*,*,#13615,.T.);
#19148=ORIENTED_EDGE('',*,*,#13616,.F.);
#19149=ORIENTED_EDGE('',*,*,#13617,.T.);
#19150=ORIENTED_EDGE('',*,*,#13618,.F.);
#19151=ORIENTED_EDGE('',*,*,#13619,.T.);
#19152=ORIENTED_EDGE('',*,*,#13620,.F.);
#19153=ORIENTED_EDGE('',*,*,#13621,.T.);
#19154=ORIENTED_EDGE('',*,*,#13622,.F.);
#19155=ORIENTED_EDGE('',*,*,#13623,.T.);
#19156=ORIENTED_EDGE('',*,*,#13624,.F.);
#19157=ORIENTED_EDGE('',*,*,#13625,.T.);
#19158=ORIENTED_EDGE('',*,*,#13626,.F.);
#19159=ORIENTED_EDGE('',*,*,#13627,.T.);
#19160=ORIENTED_EDGE('',*,*,#13628,.F.);
#19161=ORIENTED_EDGE('',*,*,#13629,.T.);
#19162=ORIENTED_EDGE('',*,*,#13630,.F.);
#19163=ORIENTED_EDGE('',*,*,#13631,.T.);
#19164=ORIENTED_EDGE('',*,*,#13632,.F.);
#19165=ORIENTED_EDGE('',*,*,#13633,.T.);
#19166=ORIENTED_EDGE('',*,*,#13634,.F.);
#19167=ORIENTED_EDGE('',*,*,#13635,.T.);
#19168=ORIENTED_EDGE('',*,*,#13636,.F.);
#19169=ORIENTED_EDGE('',*,*,#13637,.T.);
#19170=ORIENTED_EDGE('',*,*,#13638,.F.);
#19171=ORIENTED_EDGE('',*,*,#13639,.T.);
#19172=ORIENTED_EDGE('',*,*,#13640,.F.);
#19173=ORIENTED_EDGE('',*,*,#13641,.T.);
#19174=ORIENTED_EDGE('',*,*,#13642,.F.);
#19175=ORIENTED_EDGE('',*,*,#13643,.T.);
#19176=ORIENTED_EDGE('',*,*,#13644,.F.);
#19177=ORIENTED_EDGE('',*,*,#13645,.T.);
#19178=ORIENTED_EDGE('',*,*,#13646,.F.);
#19179=ORIENTED_EDGE('',*,*,#13647,.T.);
#19180=ORIENTED_EDGE('',*,*,#13648,.F.);
#19181=ORIENTED_EDGE('',*,*,#13649,.T.);
#19182=ORIENTED_EDGE('',*,*,#13650,.F.);
#19183=ORIENTED_EDGE('',*,*,#13651,.T.);
#19184=ORIENTED_EDGE('',*,*,#13652,.F.);
#19185=ORIENTED_EDGE('',*,*,#13653,.T.);
#19186=ORIENTED_EDGE('',*,*,#13654,.F.);
#19187=ORIENTED_EDGE('',*,*,#13655,.T.);
#19188=ORIENTED_EDGE('',*,*,#13656,.F.);
#19189=ORIENTED_EDGE('',*,*,#13657,.T.);
#19190=ORIENTED_EDGE('',*,*,#13658,.F.);
#19191=ORIENTED_EDGE('',*,*,#13659,.T.);
#19192=ORIENTED_EDGE('',*,*,#13660,.F.);
#19193=ORIENTED_EDGE('',*,*,#13661,.T.);
#19194=ORIENTED_EDGE('',*,*,#13662,.F.);
#19195=ORIENTED_EDGE('',*,*,#13663,.T.);
#19196=ORIENTED_EDGE('',*,*,#13664,.F.);
#19197=ORIENTED_EDGE('',*,*,#13665,.T.);
#19198=ORIENTED_EDGE('',*,*,#13666,.F.);
#19199=ORIENTED_EDGE('',*,*,#13667,.T.);
#19200=ORIENTED_EDGE('',*,*,#13668,.F.);
#19201=ORIENTED_EDGE('',*,*,#13669,.T.);
#19202=ORIENTED_EDGE('',*,*,#13670,.F.);
#19203=ORIENTED_EDGE('',*,*,#13671,.T.);
#19204=ORIENTED_EDGE('',*,*,#13672,.F.);
#19205=ORIENTED_EDGE('',*,*,#13673,.T.);
#19206=ORIENTED_EDGE('',*,*,#13674,.F.);
#19207=ORIENTED_EDGE('',*,*,#13675,.T.);
#19208=ORIENTED_EDGE('',*,*,#13676,.T.);
#19209=ORIENTED_EDGE('',*,*,#13677,.F.);
#19210=ORIENTED_EDGE('',*,*,#13678,.T.);
#19211=ORIENTED_EDGE('',*,*,#13679,.F.);
#19212=ORIENTED_EDGE('',*,*,#13611,.F.);
#19213=ORIENTED_EDGE('',*,*,#13680,.T.);
#19214=ORIENTED_EDGE('',*,*,#13540,.T.);
#19215=ORIENTED_EDGE('',*,*,#13680,.F.);
#19216=ORIENTED_EDGE('',*,*,#13609,.T.);
#19217=ORIENTED_EDGE('',*,*,#13681,.T.);
#19218=ORIENTED_EDGE('',*,*,#13538,.F.);
#19219=ORIENTED_EDGE('',*,*,#13681,.F.);
#19220=ORIENTED_EDGE('',*,*,#13614,.T.);
#19221=ORIENTED_EDGE('',*,*,#13682,.T.);
#19222=ORIENTED_EDGE('',*,*,#13543,.T.);
#19223=ORIENTED_EDGE('',*,*,#13683,.T.);
#19224=ORIENTED_EDGE('',*,*,#13684,.F.);
#19225=ORIENTED_EDGE('',*,*,#13685,.T.);
#19226=ORIENTED_EDGE('',*,*,#13615,.F.);
#19227=ORIENTED_EDGE('',*,*,#13682,.F.);
#19228=ORIENTED_EDGE('',*,*,#13613,.F.);
#19229=ORIENTED_EDGE('',*,*,#13686,.T.);
#19230=ORIENTED_EDGE('',*,*,#13542,.F.);
#19231=ORIENTED_EDGE('',*,*,#13687,.T.);
#19232=ORIENTED_EDGE('',*,*,#13688,.F.);
#19233=ORIENTED_EDGE('',*,*,#13689,.F.);
#19234=ORIENTED_EDGE('',*,*,#13683,.F.);
#19235=ORIENTED_EDGE('',*,*,#13612,.T.);
#19236=ORIENTED_EDGE('',*,*,#13686,.F.);
#19237=ORIENTED_EDGE('',*,*,#13618,.T.);
#19238=ORIENTED_EDGE('',*,*,#13690,.T.);
#19239=ORIENTED_EDGE('',*,*,#13547,.T.);
#19240=ORIENTED_EDGE('',*,*,#13691,.T.);
#19241=ORIENTED_EDGE('',*,*,#13692,.F.);
#19242=ORIENTED_EDGE('',*,*,#13693,.T.);
#19243=ORIENTED_EDGE('',*,*,#13619,.F.);
#19244=ORIENTED_EDGE('',*,*,#13690,.F.);
#19245=ORIENTED_EDGE('',*,*,#13617,.F.);
#19246=ORIENTED_EDGE('',*,*,#13694,.T.);
#19247=ORIENTED_EDGE('',*,*,#13546,.F.);
#19248=ORIENTED_EDGE('',*,*,#13695,.T.);
#19249=ORIENTED_EDGE('',*,*,#13696,.F.);
#19250=ORIENTED_EDGE('',*,*,#13697,.F.);
#19251=ORIENTED_EDGE('',*,*,#13691,.F.);
#19252=ORIENTED_EDGE('',*,*,#13616,.T.);
#19253=ORIENTED_EDGE('',*,*,#13694,.F.);
#19254=ORIENTED_EDGE('',*,*,#13622,.T.);
#19255=ORIENTED_EDGE('',*,*,#13698,.T.);
#19256=ORIENTED_EDGE('',*,*,#13551,.T.);
#19257=ORIENTED_EDGE('',*,*,#13699,.T.);
#19258=ORIENTED_EDGE('',*,*,#13700,.F.);
#19259=ORIENTED_EDGE('',*,*,#13701,.T.);
#19260=ORIENTED_EDGE('',*,*,#13623,.F.);
#19261=ORIENTED_EDGE('',*,*,#13698,.F.);
#19262=ORIENTED_EDGE('',*,*,#13621,.F.);
#19263=ORIENTED_EDGE('',*,*,#13702,.T.);
#19264=ORIENTED_EDGE('',*,*,#13550,.F.);
#19265=ORIENTED_EDGE('',*,*,#13703,.T.);
#19266=ORIENTED_EDGE('',*,*,#13704,.F.);
#19267=ORIENTED_EDGE('',*,*,#13705,.F.);
#19268=ORIENTED_EDGE('',*,*,#13699,.F.);
#19269=ORIENTED_EDGE('',*,*,#13620,.T.);
#19270=ORIENTED_EDGE('',*,*,#13702,.F.);
#19271=ORIENTED_EDGE('',*,*,#13626,.T.);
#19272=ORIENTED_EDGE('',*,*,#13706,.T.);
#19273=ORIENTED_EDGE('',*,*,#13555,.T.);
#19274=ORIENTED_EDGE('',*,*,#13707,.T.);
#19275=ORIENTED_EDGE('',*,*,#13708,.F.);
#19276=ORIENTED_EDGE('',*,*,#13709,.T.);
#19277=ORIENTED_EDGE('',*,*,#13627,.F.);
#19278=ORIENTED_EDGE('',*,*,#13706,.F.);
#19279=ORIENTED_EDGE('',*,*,#13625,.F.);
#19280=ORIENTED_EDGE('',*,*,#13710,.T.);
#19281=ORIENTED_EDGE('',*,*,#13554,.F.);
#19282=ORIENTED_EDGE('',*,*,#13711,.T.);
#19283=ORIENTED_EDGE('',*,*,#13712,.F.);
#19284=ORIENTED_EDGE('',*,*,#13713,.F.);
#19285=ORIENTED_EDGE('',*,*,#13707,.F.);
#19286=ORIENTED_EDGE('',*,*,#13624,.T.);
#19287=ORIENTED_EDGE('',*,*,#13710,.F.);
#19288=ORIENTED_EDGE('',*,*,#13630,.T.);
#19289=ORIENTED_EDGE('',*,*,#13714,.T.);
#19290=ORIENTED_EDGE('',*,*,#13559,.T.);
#19291=ORIENTED_EDGE('',*,*,#13715,.T.);
#19292=ORIENTED_EDGE('',*,*,#13716,.F.);
#19293=ORIENTED_EDGE('',*,*,#13717,.T.);
#19294=ORIENTED_EDGE('',*,*,#13631,.F.);
#19295=ORIENTED_EDGE('',*,*,#13714,.F.);
#19296=ORIENTED_EDGE('',*,*,#13629,.F.);
#19297=ORIENTED_EDGE('',*,*,#13718,.T.);
#19298=ORIENTED_EDGE('',*,*,#13558,.F.);
#19299=ORIENTED_EDGE('',*,*,#13719,.T.);
#19300=ORIENTED_EDGE('',*,*,#13720,.F.);
#19301=ORIENTED_EDGE('',*,*,#13721,.F.);
#19302=ORIENTED_EDGE('',*,*,#13715,.F.);
#19303=ORIENTED_EDGE('',*,*,#13628,.T.);
#19304=ORIENTED_EDGE('',*,*,#13718,.F.);
#19305=ORIENTED_EDGE('',*,*,#13634,.T.);
#19306=ORIENTED_EDGE('',*,*,#13722,.T.);
#19307=ORIENTED_EDGE('',*,*,#13563,.T.);
#19308=ORIENTED_EDGE('',*,*,#13723,.T.);
#19309=ORIENTED_EDGE('',*,*,#13724,.F.);
#19310=ORIENTED_EDGE('',*,*,#13725,.T.);
#19311=ORIENTED_EDGE('',*,*,#13635,.F.);
#19312=ORIENTED_EDGE('',*,*,#13722,.F.);
#19313=ORIENTED_EDGE('',*,*,#13633,.F.);
#19314=ORIENTED_EDGE('',*,*,#13726,.T.);
#19315=ORIENTED_EDGE('',*,*,#13562,.F.);
#19316=ORIENTED_EDGE('',*,*,#13727,.T.);
#19317=ORIENTED_EDGE('',*,*,#13728,.F.);
#19318=ORIENTED_EDGE('',*,*,#13729,.F.);
#19319=ORIENTED_EDGE('',*,*,#13723,.F.);
#19320=ORIENTED_EDGE('',*,*,#13632,.T.);
#19321=ORIENTED_EDGE('',*,*,#13726,.F.);
#19322=ORIENTED_EDGE('',*,*,#13638,.T.);
#19323=ORIENTED_EDGE('',*,*,#13730,.T.);
#19324=ORIENTED_EDGE('',*,*,#13567,.T.);
#19325=ORIENTED_EDGE('',*,*,#13731,.T.);
#19326=ORIENTED_EDGE('',*,*,#13732,.F.);
#19327=ORIENTED_EDGE('',*,*,#13733,.T.);
#19328=ORIENTED_EDGE('',*,*,#13639,.F.);
#19329=ORIENTED_EDGE('',*,*,#13730,.F.);
#19330=ORIENTED_EDGE('',*,*,#13637,.F.);
#19331=ORIENTED_EDGE('',*,*,#13734,.T.);
#19332=ORIENTED_EDGE('',*,*,#13566,.F.);
#19333=ORIENTED_EDGE('',*,*,#13735,.T.);
#19334=ORIENTED_EDGE('',*,*,#13736,.F.);
#19335=ORIENTED_EDGE('',*,*,#13737,.F.);
#19336=ORIENTED_EDGE('',*,*,#13731,.F.);
#19337=ORIENTED_EDGE('',*,*,#13636,.T.);
#19338=ORIENTED_EDGE('',*,*,#13734,.F.);
#19339=ORIENTED_EDGE('',*,*,#13642,.T.);
#19340=ORIENTED_EDGE('',*,*,#13738,.T.);
#19341=ORIENTED_EDGE('',*,*,#13571,.T.);
#19342=ORIENTED_EDGE('',*,*,#13739,.T.);
#19343=ORIENTED_EDGE('',*,*,#13740,.F.);
#19344=ORIENTED_EDGE('',*,*,#13741,.T.);
#19345=ORIENTED_EDGE('',*,*,#13643,.F.);
#19346=ORIENTED_EDGE('',*,*,#13738,.F.);
#19347=ORIENTED_EDGE('',*,*,#13641,.F.);
#19348=ORIENTED_EDGE('',*,*,#13742,.T.);
#19349=ORIENTED_EDGE('',*,*,#13570,.F.);
#19350=ORIENTED_EDGE('',*,*,#13743,.T.);
#19351=ORIENTED_EDGE('',*,*,#13744,.F.);
#19352=ORIENTED_EDGE('',*,*,#13745,.F.);
#19353=ORIENTED_EDGE('',*,*,#13739,.F.);
#19354=ORIENTED_EDGE('',*,*,#13640,.T.);
#19355=ORIENTED_EDGE('',*,*,#13742,.F.);
#19356=ORIENTED_EDGE('',*,*,#13646,.T.);
#19357=ORIENTED_EDGE('',*,*,#13746,.T.);
#19358=ORIENTED_EDGE('',*,*,#13575,.T.);
#19359=ORIENTED_EDGE('',*,*,#13747,.T.);
#19360=ORIENTED_EDGE('',*,*,#13748,.F.);
#19361=ORIENTED_EDGE('',*,*,#13749,.T.);
#19362=ORIENTED_EDGE('',*,*,#13647,.F.);
#19363=ORIENTED_EDGE('',*,*,#13746,.F.);
#19364=ORIENTED_EDGE('',*,*,#13645,.F.);
#19365=ORIENTED_EDGE('',*,*,#13750,.T.);
#19366=ORIENTED_EDGE('',*,*,#13574,.F.);
#19367=ORIENTED_EDGE('',*,*,#13751,.T.);
#19368=ORIENTED_EDGE('',*,*,#13752,.F.);
#19369=ORIENTED_EDGE('',*,*,#13753,.F.);
#19370=ORIENTED_EDGE('',*,*,#13747,.F.);
#19371=ORIENTED_EDGE('',*,*,#13644,.T.);
#19372=ORIENTED_EDGE('',*,*,#13750,.F.);
#19373=ORIENTED_EDGE('',*,*,#13650,.T.);
#19374=ORIENTED_EDGE('',*,*,#13754,.T.);
#19375=ORIENTED_EDGE('',*,*,#13579,.T.);
#19376=ORIENTED_EDGE('',*,*,#13755,.T.);
#19377=ORIENTED_EDGE('',*,*,#13756,.F.);
#19378=ORIENTED_EDGE('',*,*,#13757,.T.);
#19379=ORIENTED_EDGE('',*,*,#13651,.F.);
#19380=ORIENTED_EDGE('',*,*,#13754,.F.);
#19381=ORIENTED_EDGE('',*,*,#13649,.F.);
#19382=ORIENTED_EDGE('',*,*,#13758,.T.);
#19383=ORIENTED_EDGE('',*,*,#13578,.F.);
#19384=ORIENTED_EDGE('',*,*,#13759,.T.);
#19385=ORIENTED_EDGE('',*,*,#13760,.F.);
#19386=ORIENTED_EDGE('',*,*,#13761,.F.);
#19387=ORIENTED_EDGE('',*,*,#13755,.F.);
#19388=ORIENTED_EDGE('',*,*,#13648,.T.);
#19389=ORIENTED_EDGE('',*,*,#13758,.F.);
#19390=ORIENTED_EDGE('',*,*,#13654,.T.);
#19391=ORIENTED_EDGE('',*,*,#13762,.T.);
#19392=ORIENTED_EDGE('',*,*,#13583,.T.);
#19393=ORIENTED_EDGE('',*,*,#13763,.T.);
#19394=ORIENTED_EDGE('',*,*,#13764,.F.);
#19395=ORIENTED_EDGE('',*,*,#13765,.T.);
#19396=ORIENTED_EDGE('',*,*,#13655,.F.);
#19397=ORIENTED_EDGE('',*,*,#13762,.F.);
#19398=ORIENTED_EDGE('',*,*,#13653,.F.);
#19399=ORIENTED_EDGE('',*,*,#13766,.T.);
#19400=ORIENTED_EDGE('',*,*,#13582,.F.);
#19401=ORIENTED_EDGE('',*,*,#13767,.T.);
#19402=ORIENTED_EDGE('',*,*,#13768,.F.);
#19403=ORIENTED_EDGE('',*,*,#13769,.F.);
#19404=ORIENTED_EDGE('',*,*,#13763,.F.);
#19405=ORIENTED_EDGE('',*,*,#13652,.T.);
#19406=ORIENTED_EDGE('',*,*,#13766,.F.);
#19407=ORIENTED_EDGE('',*,*,#13658,.T.);
#19408=ORIENTED_EDGE('',*,*,#13770,.T.);
#19409=ORIENTED_EDGE('',*,*,#13587,.T.);
#19410=ORIENTED_EDGE('',*,*,#13771,.T.);
#19411=ORIENTED_EDGE('',*,*,#13772,.F.);
#19412=ORIENTED_EDGE('',*,*,#13773,.T.);
#19413=ORIENTED_EDGE('',*,*,#13659,.F.);
#19414=ORIENTED_EDGE('',*,*,#13770,.F.);
#19415=ORIENTED_EDGE('',*,*,#13657,.F.);
#19416=ORIENTED_EDGE('',*,*,#13774,.T.);
#19417=ORIENTED_EDGE('',*,*,#13586,.F.);
#19418=ORIENTED_EDGE('',*,*,#13775,.T.);
#19419=ORIENTED_EDGE('',*,*,#13776,.F.);
#19420=ORIENTED_EDGE('',*,*,#13777,.F.);
#19421=ORIENTED_EDGE('',*,*,#13771,.F.);
#19422=ORIENTED_EDGE('',*,*,#13656,.T.);
#19423=ORIENTED_EDGE('',*,*,#13774,.F.);
#19424=ORIENTED_EDGE('',*,*,#13662,.T.);
#19425=ORIENTED_EDGE('',*,*,#13778,.T.);
#19426=ORIENTED_EDGE('',*,*,#13591,.T.);
#19427=ORIENTED_EDGE('',*,*,#13779,.T.);
#19428=ORIENTED_EDGE('',*,*,#13780,.F.);
#19429=ORIENTED_EDGE('',*,*,#13781,.T.);
#19430=ORIENTED_EDGE('',*,*,#13663,.F.);
#19431=ORIENTED_EDGE('',*,*,#13778,.F.);
#19432=ORIENTED_EDGE('',*,*,#13661,.F.);
#19433=ORIENTED_EDGE('',*,*,#13782,.T.);
#19434=ORIENTED_EDGE('',*,*,#13590,.F.);
#19435=ORIENTED_EDGE('',*,*,#13783,.T.);
#19436=ORIENTED_EDGE('',*,*,#13784,.F.);
#19437=ORIENTED_EDGE('',*,*,#13785,.F.);
#19438=ORIENTED_EDGE('',*,*,#13779,.F.);
#19439=ORIENTED_EDGE('',*,*,#13660,.T.);
#19440=ORIENTED_EDGE('',*,*,#13782,.F.);
#19441=ORIENTED_EDGE('',*,*,#13666,.T.);
#19442=ORIENTED_EDGE('',*,*,#13786,.T.);
#19443=ORIENTED_EDGE('',*,*,#13595,.T.);
#19444=ORIENTED_EDGE('',*,*,#13787,.T.);
#19445=ORIENTED_EDGE('',*,*,#13788,.F.);
#19446=ORIENTED_EDGE('',*,*,#13789,.T.);
#19447=ORIENTED_EDGE('',*,*,#13667,.F.);
#19448=ORIENTED_EDGE('',*,*,#13786,.F.);
#19449=ORIENTED_EDGE('',*,*,#13665,.F.);
#19450=ORIENTED_EDGE('',*,*,#13790,.T.);
#19451=ORIENTED_EDGE('',*,*,#13594,.F.);
#19452=ORIENTED_EDGE('',*,*,#13791,.T.);
#19453=ORIENTED_EDGE('',*,*,#13792,.F.);
#19454=ORIENTED_EDGE('',*,*,#13793,.F.);
#19455=ORIENTED_EDGE('',*,*,#13787,.F.);
#19456=ORIENTED_EDGE('',*,*,#13664,.T.);
#19457=ORIENTED_EDGE('',*,*,#13790,.F.);
#19458=ORIENTED_EDGE('',*,*,#13670,.T.);
#19459=ORIENTED_EDGE('',*,*,#13794,.T.);
#19460=ORIENTED_EDGE('',*,*,#13599,.T.);
#19461=ORIENTED_EDGE('',*,*,#13795,.T.);
#19462=ORIENTED_EDGE('',*,*,#13796,.F.);
#19463=ORIENTED_EDGE('',*,*,#13797,.T.);
#19464=ORIENTED_EDGE('',*,*,#13671,.F.);
#19465=ORIENTED_EDGE('',*,*,#13794,.F.);
#19466=ORIENTED_EDGE('',*,*,#13669,.F.);
#19467=ORIENTED_EDGE('',*,*,#13798,.T.);
#19468=ORIENTED_EDGE('',*,*,#13598,.F.);
#19469=ORIENTED_EDGE('',*,*,#13799,.T.);
#19470=ORIENTED_EDGE('',*,*,#13800,.F.);
#19471=ORIENTED_EDGE('',*,*,#13801,.F.);
#19472=ORIENTED_EDGE('',*,*,#13795,.F.);
#19473=ORIENTED_EDGE('',*,*,#13668,.T.);
#19474=ORIENTED_EDGE('',*,*,#13798,.F.);
#19475=ORIENTED_EDGE('',*,*,#13674,.T.);
#19476=ORIENTED_EDGE('',*,*,#13802,.T.);
#19477=ORIENTED_EDGE('',*,*,#13603,.T.);
#19478=ORIENTED_EDGE('',*,*,#13803,.T.);
#19479=ORIENTED_EDGE('',*,*,#13804,.F.);
#19480=ORIENTED_EDGE('',*,*,#13805,.T.);
#19481=ORIENTED_EDGE('',*,*,#13675,.F.);
#19482=ORIENTED_EDGE('',*,*,#13802,.F.);
#19483=ORIENTED_EDGE('',*,*,#13673,.F.);
#19484=ORIENTED_EDGE('',*,*,#13806,.T.);
#19485=ORIENTED_EDGE('',*,*,#13602,.F.);
#19486=ORIENTED_EDGE('',*,*,#13807,.T.);
#19487=ORIENTED_EDGE('',*,*,#13808,.F.);
#19488=ORIENTED_EDGE('',*,*,#13809,.F.);
#19489=ORIENTED_EDGE('',*,*,#13803,.F.);
#19490=ORIENTED_EDGE('',*,*,#13672,.T.);
#19491=ORIENTED_EDGE('',*,*,#13806,.F.);
#19492=ORIENTED_EDGE('',*,*,#13677,.T.);
#19493=ORIENTED_EDGE('',*,*,#13810,.F.);
#19494=ORIENTED_EDGE('',*,*,#13679,.T.);
#19495=ORIENTED_EDGE('',*,*,#13811,.T.);
#19496=ORIENTED_EDGE('',*,*,#13606,.T.);
#19497=ORIENTED_EDGE('',*,*,#13812,.T.);
#19498=ORIENTED_EDGE('',*,*,#13813,.F.);
#19499=ORIENTED_EDGE('',*,*,#13814,.T.);
#19500=ORIENTED_EDGE('',*,*,#13678,.F.);
#19501=ORIENTED_EDGE('',*,*,#13810,.T.);
#19502=ORIENTED_EDGE('',*,*,#13676,.F.);
#19503=ORIENTED_EDGE('',*,*,#13811,.F.);
#19504=ORIENTED_EDGE('',*,*,#13605,.F.);
#19505=ORIENTED_EDGE('',*,*,#13815,.T.);
#19506=ORIENTED_EDGE('',*,*,#13816,.F.);
#19507=ORIENTED_EDGE('',*,*,#13817,.F.);
#19508=ORIENTED_EDGE('',*,*,#13812,.F.);
#19509=ORIENTED_EDGE('',*,*,#13541,.T.);
#19510=ORIENTED_EDGE('',*,*,#13818,.F.);
#19511=ORIENTED_EDGE('',*,*,#13819,.F.);
#19512=ORIENTED_EDGE('',*,*,#13687,.F.);
#19513=ORIENTED_EDGE('',*,*,#13544,.F.);
#19514=ORIENTED_EDGE('',*,*,#13685,.F.);
#19515=ORIENTED_EDGE('',*,*,#13820,.F.);
#19516=ORIENTED_EDGE('',*,*,#13821,.F.);
#19517=ORIENTED_EDGE('',*,*,#13818,.T.);
#19518=ORIENTED_EDGE('',*,*,#13822,.F.);
#19519=ORIENTED_EDGE('',*,*,#13823,.T.);
#19520=ORIENTED_EDGE('',*,*,#13824,.T.);
#19521=ORIENTED_EDGE('',*,*,#13825,.T.);
#19522=ORIENTED_EDGE('',*,*,#13740,.T.);
#19523=ORIENTED_EDGE('',*,*,#13745,.T.);
#19524=ORIENTED_EDGE('',*,*,#13826,.T.);
#19525=ORIENTED_EDGE('',*,*,#13827,.T.);
#19526=ORIENTED_EDGE('',*,*,#13732,.T.);
#19527=ORIENTED_EDGE('',*,*,#13737,.T.);
#19528=ORIENTED_EDGE('',*,*,#13828,.T.);
#19529=ORIENTED_EDGE('',*,*,#13829,.T.);
#19530=ORIENTED_EDGE('',*,*,#13724,.T.);
#19531=ORIENTED_EDGE('',*,*,#13729,.T.);
#19532=ORIENTED_EDGE('',*,*,#13830,.T.);
#19533=ORIENTED_EDGE('',*,*,#13831,.T.);
#19534=ORIENTED_EDGE('',*,*,#13716,.T.);
#19535=ORIENTED_EDGE('',*,*,#13721,.T.);
#19536=ORIENTED_EDGE('',*,*,#13832,.T.);
#19537=ORIENTED_EDGE('',*,*,#13833,.T.);
#19538=ORIENTED_EDGE('',*,*,#13708,.T.);
#19539=ORIENTED_EDGE('',*,*,#13713,.T.);
#19540=ORIENTED_EDGE('',*,*,#13834,.T.);
#19541=ORIENTED_EDGE('',*,*,#13835,.T.);
#19542=ORIENTED_EDGE('',*,*,#13700,.T.);
#19543=ORIENTED_EDGE('',*,*,#13705,.T.);
#19544=ORIENTED_EDGE('',*,*,#13836,.T.);
#19545=ORIENTED_EDGE('',*,*,#13837,.T.);
#19546=ORIENTED_EDGE('',*,*,#13692,.T.);
#19547=ORIENTED_EDGE('',*,*,#13697,.T.);
#19548=ORIENTED_EDGE('',*,*,#13838,.T.);
#19549=ORIENTED_EDGE('',*,*,#13820,.T.);
#19550=ORIENTED_EDGE('',*,*,#13684,.T.);
#19551=ORIENTED_EDGE('',*,*,#13689,.T.);
#19552=ORIENTED_EDGE('',*,*,#13839,.T.);
#19553=ORIENTED_EDGE('',*,*,#13840,.T.);
#19554=ORIENTED_EDGE('',*,*,#13813,.T.);
#19555=ORIENTED_EDGE('',*,*,#13817,.T.);
#19556=ORIENTED_EDGE('',*,*,#13841,.T.);
#19557=ORIENTED_EDGE('',*,*,#13842,.T.);
#19558=ORIENTED_EDGE('',*,*,#13804,.T.);
#19559=ORIENTED_EDGE('',*,*,#13809,.T.);
#19560=ORIENTED_EDGE('',*,*,#13843,.T.);
#19561=ORIENTED_EDGE('',*,*,#13844,.T.);
#19562=ORIENTED_EDGE('',*,*,#13796,.T.);
#19563=ORIENTED_EDGE('',*,*,#13801,.T.);
#19564=ORIENTED_EDGE('',*,*,#13845,.T.);
#19565=ORIENTED_EDGE('',*,*,#13846,.T.);
#19566=ORIENTED_EDGE('',*,*,#13788,.T.);
#19567=ORIENTED_EDGE('',*,*,#13793,.T.);
#19568=ORIENTED_EDGE('',*,*,#13847,.T.);
#19569=ORIENTED_EDGE('',*,*,#13848,.T.);
#19570=ORIENTED_EDGE('',*,*,#13780,.T.);
#19571=ORIENTED_EDGE('',*,*,#13785,.T.);
#19572=ORIENTED_EDGE('',*,*,#13849,.T.);
#19573=ORIENTED_EDGE('',*,*,#13850,.T.);
#19574=ORIENTED_EDGE('',*,*,#13772,.T.);
#19575=ORIENTED_EDGE('',*,*,#13777,.T.);
#19576=ORIENTED_EDGE('',*,*,#13851,.T.);
#19577=ORIENTED_EDGE('',*,*,#13852,.T.);
#19578=ORIENTED_EDGE('',*,*,#13764,.T.);
#19579=ORIENTED_EDGE('',*,*,#13769,.T.);
#19580=ORIENTED_EDGE('',*,*,#13853,.T.);
#19581=ORIENTED_EDGE('',*,*,#13854,.T.);
#19582=ORIENTED_EDGE('',*,*,#13756,.T.);
#19583=ORIENTED_EDGE('',*,*,#13761,.T.);
#19584=ORIENTED_EDGE('',*,*,#13855,.T.);
#19585=ORIENTED_EDGE('',*,*,#13856,.T.);
#19586=ORIENTED_EDGE('',*,*,#13748,.T.);
#19587=ORIENTED_EDGE('',*,*,#13753,.T.);
#19588=ORIENTED_EDGE('',*,*,#13857,.T.);
#19589=ORIENTED_EDGE('',*,*,#13823,.F.);
#19590=ORIENTED_EDGE('',*,*,#13545,.T.);
#19591=ORIENTED_EDGE('',*,*,#13858,.F.);
#19592=ORIENTED_EDGE('',*,*,#13859,.F.);
#19593=ORIENTED_EDGE('',*,*,#13695,.F.);
#19594=ORIENTED_EDGE('',*,*,#13548,.F.);
#19595=ORIENTED_EDGE('',*,*,#13693,.F.);
#19596=ORIENTED_EDGE('',*,*,#13837,.F.);
#19597=ORIENTED_EDGE('',*,*,#13860,.F.);
#19598=ORIENTED_EDGE('',*,*,#13858,.T.);
#19599=ORIENTED_EDGE('',*,*,#13549,.T.);
#19600=ORIENTED_EDGE('',*,*,#13861,.F.);
#19601=ORIENTED_EDGE('',*,*,#13862,.F.);
#19602=ORIENTED_EDGE('',*,*,#13703,.F.);
#19603=ORIENTED_EDGE('',*,*,#13552,.F.);
#19604=ORIENTED_EDGE('',*,*,#13701,.F.);
#19605=ORIENTED_EDGE('',*,*,#13835,.F.);
#19606=ORIENTED_EDGE('',*,*,#13863,.F.);
#19607=ORIENTED_EDGE('',*,*,#13861,.T.);
#19608=ORIENTED_EDGE('',*,*,#13553,.T.);
#19609=ORIENTED_EDGE('',*,*,#13864,.F.);
#19610=ORIENTED_EDGE('',*,*,#13865,.F.);
#19611=ORIENTED_EDGE('',*,*,#13711,.F.);
#19612=ORIENTED_EDGE('',*,*,#13556,.F.);
#19613=ORIENTED_EDGE('',*,*,#13709,.F.);
#19614=ORIENTED_EDGE('',*,*,#13833,.F.);
#19615=ORIENTED_EDGE('',*,*,#13866,.F.);
#19616=ORIENTED_EDGE('',*,*,#13864,.T.);
#19617=ORIENTED_EDGE('',*,*,#13557,.T.);
#19618=ORIENTED_EDGE('',*,*,#13867,.F.);
#19619=ORIENTED_EDGE('',*,*,#13868,.F.);
#19620=ORIENTED_EDGE('',*,*,#13719,.F.);
#19621=ORIENTED_EDGE('',*,*,#13560,.F.);
#19622=ORIENTED_EDGE('',*,*,#13717,.F.);
#19623=ORIENTED_EDGE('',*,*,#13831,.F.);
#19624=ORIENTED_EDGE('',*,*,#13869,.F.);
#19625=ORIENTED_EDGE('',*,*,#13867,.T.);
#19626=ORIENTED_EDGE('',*,*,#13561,.T.);
#19627=ORIENTED_EDGE('',*,*,#13870,.F.);
#19628=ORIENTED_EDGE('',*,*,#13871,.F.);
#19629=ORIENTED_EDGE('',*,*,#13727,.F.);
#19630=ORIENTED_EDGE('',*,*,#13564,.F.);
#19631=ORIENTED_EDGE('',*,*,#13725,.F.);
#19632=ORIENTED_EDGE('',*,*,#13829,.F.);
#19633=ORIENTED_EDGE('',*,*,#13872,.F.);
#19634=ORIENTED_EDGE('',*,*,#13870,.T.);
#19635=ORIENTED_EDGE('',*,*,#13565,.T.);
#19636=ORIENTED_EDGE('',*,*,#13873,.F.);
#19637=ORIENTED_EDGE('',*,*,#13874,.F.);
#19638=ORIENTED_EDGE('',*,*,#13735,.F.);
#19639=ORIENTED_EDGE('',*,*,#13568,.F.);
#19640=ORIENTED_EDGE('',*,*,#13733,.F.);
#19641=ORIENTED_EDGE('',*,*,#13827,.F.);
#19642=ORIENTED_EDGE('',*,*,#13875,.F.);
#19643=ORIENTED_EDGE('',*,*,#13873,.T.);
#19644=ORIENTED_EDGE('',*,*,#13569,.T.);
#19645=ORIENTED_EDGE('',*,*,#13876,.F.);
#19646=ORIENTED_EDGE('',*,*,#13877,.F.);
#19647=ORIENTED_EDGE('',*,*,#13743,.F.);
#19648=ORIENTED_EDGE('',*,*,#13572,.F.);
#19649=ORIENTED_EDGE('',*,*,#13741,.F.);
#19650=ORIENTED_EDGE('',*,*,#13825,.F.);
#19651=ORIENTED_EDGE('',*,*,#13878,.F.);
#19652=ORIENTED_EDGE('',*,*,#13876,.T.);
#19653=ORIENTED_EDGE('',*,*,#13573,.T.);
#19654=ORIENTED_EDGE('',*,*,#13879,.F.);
#19655=ORIENTED_EDGE('',*,*,#13880,.F.);
#19656=ORIENTED_EDGE('',*,*,#13751,.F.);
#19657=ORIENTED_EDGE('',*,*,#13576,.F.);
#19658=ORIENTED_EDGE('',*,*,#13749,.F.);
#19659=ORIENTED_EDGE('',*,*,#13856,.F.);
#19660=ORIENTED_EDGE('',*,*,#13881,.F.);
#19661=ORIENTED_EDGE('',*,*,#13879,.T.);
#19662=ORIENTED_EDGE('',*,*,#13577,.T.);
#19663=ORIENTED_EDGE('',*,*,#13882,.F.);
#19664=ORIENTED_EDGE('',*,*,#13883,.F.);
#19665=ORIENTED_EDGE('',*,*,#13759,.F.);
#19666=ORIENTED_EDGE('',*,*,#13580,.F.);
#19667=ORIENTED_EDGE('',*,*,#13757,.F.);
#19668=ORIENTED_EDGE('',*,*,#13854,.F.);
#19669=ORIENTED_EDGE('',*,*,#13884,.F.);
#19670=ORIENTED_EDGE('',*,*,#13882,.T.);
#19671=ORIENTED_EDGE('',*,*,#13581,.T.);
#19672=ORIENTED_EDGE('',*,*,#13885,.F.);
#19673=ORIENTED_EDGE('',*,*,#13886,.F.);
#19674=ORIENTED_EDGE('',*,*,#13767,.F.);
#19675=ORIENTED_EDGE('',*,*,#13584,.F.);
#19676=ORIENTED_EDGE('',*,*,#13765,.F.);
#19677=ORIENTED_EDGE('',*,*,#13852,.F.);
#19678=ORIENTED_EDGE('',*,*,#13887,.F.);
#19679=ORIENTED_EDGE('',*,*,#13885,.T.);
#19680=ORIENTED_EDGE('',*,*,#13585,.T.);
#19681=ORIENTED_EDGE('',*,*,#13888,.F.);
#19682=ORIENTED_EDGE('',*,*,#13889,.F.);
#19683=ORIENTED_EDGE('',*,*,#13775,.F.);
#19684=ORIENTED_EDGE('',*,*,#13588,.F.);
#19685=ORIENTED_EDGE('',*,*,#13773,.F.);
#19686=ORIENTED_EDGE('',*,*,#13850,.F.);
#19687=ORIENTED_EDGE('',*,*,#13890,.F.);
#19688=ORIENTED_EDGE('',*,*,#13888,.T.);
#19689=ORIENTED_EDGE('',*,*,#13589,.T.);
#19690=ORIENTED_EDGE('',*,*,#13891,.F.);
#19691=ORIENTED_EDGE('',*,*,#13892,.F.);
#19692=ORIENTED_EDGE('',*,*,#13783,.F.);
#19693=ORIENTED_EDGE('',*,*,#13592,.F.);
#19694=ORIENTED_EDGE('',*,*,#13781,.F.);
#19695=ORIENTED_EDGE('',*,*,#13848,.F.);
#19696=ORIENTED_EDGE('',*,*,#13893,.F.);
#19697=ORIENTED_EDGE('',*,*,#13891,.T.);
#19698=ORIENTED_EDGE('',*,*,#13593,.T.);
#19699=ORIENTED_EDGE('',*,*,#13894,.F.);
#19700=ORIENTED_EDGE('',*,*,#13895,.F.);
#19701=ORIENTED_EDGE('',*,*,#13791,.F.);
#19702=ORIENTED_EDGE('',*,*,#13596,.F.);
#19703=ORIENTED_EDGE('',*,*,#13789,.F.);
#19704=ORIENTED_EDGE('',*,*,#13846,.F.);
#19705=ORIENTED_EDGE('',*,*,#13896,.F.);
#19706=ORIENTED_EDGE('',*,*,#13894,.T.);
#19707=ORIENTED_EDGE('',*,*,#13597,.T.);
#19708=ORIENTED_EDGE('',*,*,#13897,.F.);
#19709=ORIENTED_EDGE('',*,*,#13898,.F.);
#19710=ORIENTED_EDGE('',*,*,#13799,.F.);
#19711=ORIENTED_EDGE('',*,*,#13600,.F.);
#19712=ORIENTED_EDGE('',*,*,#13797,.F.);
#19713=ORIENTED_EDGE('',*,*,#13844,.F.);
#19714=ORIENTED_EDGE('',*,*,#13899,.F.);
#19715=ORIENTED_EDGE('',*,*,#13897,.T.);
#19716=ORIENTED_EDGE('',*,*,#13601,.T.);
#19717=ORIENTED_EDGE('',*,*,#13900,.F.);
#19718=ORIENTED_EDGE('',*,*,#13901,.F.);
#19719=ORIENTED_EDGE('',*,*,#13807,.F.);
#19720=ORIENTED_EDGE('',*,*,#13604,.F.);
#19721=ORIENTED_EDGE('',*,*,#13805,.F.);
#19722=ORIENTED_EDGE('',*,*,#13842,.F.);
#19723=ORIENTED_EDGE('',*,*,#13902,.F.);
#19724=ORIENTED_EDGE('',*,*,#13900,.T.);
#19725=ORIENTED_EDGE('',*,*,#13607,.F.);
#19726=ORIENTED_EDGE('',*,*,#13814,.F.);
#19727=ORIENTED_EDGE('',*,*,#13840,.F.);
#19728=ORIENTED_EDGE('',*,*,#13903,.F.);
#19729=ORIENTED_EDGE('',*,*,#13904,.T.);
#19730=ORIENTED_EDGE('',*,*,#13608,.T.);
#19731=ORIENTED_EDGE('',*,*,#13904,.F.);
#19732=ORIENTED_EDGE('',*,*,#13905,.F.);
#19733=ORIENTED_EDGE('',*,*,#13815,.F.);
#19734=ORIENTED_EDGE('',*,*,#13906,.T.);
#19735=ORIENTED_EDGE('',*,*,#13907,.T.);
#19736=ORIENTED_EDGE('',*,*,#13908,.F.);
#19737=ORIENTED_EDGE('',*,*,#13907,.F.);
#19738=ORIENTED_EDGE('',*,*,#13909,.F.);
#19739=ORIENTED_EDGE('',*,*,#13908,.T.);
#19740=ORIENTED_EDGE('',*,*,#13910,.F.);
#19741=ORIENTED_EDGE('',*,*,#13911,.T.);
#19742=ORIENTED_EDGE('',*,*,#13909,.T.);
#19743=ORIENTED_EDGE('',*,*,#13911,.F.);
#19744=ORIENTED_EDGE('',*,*,#13912,.F.);
#19745=ORIENTED_EDGE('',*,*,#13913,.T.);
#19746=ORIENTED_EDGE('',*,*,#13910,.T.);
#19747=ORIENTED_EDGE('',*,*,#13913,.F.);
#19748=ORIENTED_EDGE('',*,*,#13912,.T.);
#19749=ORIENTED_EDGE('',*,*,#13821,.T.);
#19750=ORIENTED_EDGE('',*,*,#13838,.F.);
#19751=ORIENTED_EDGE('',*,*,#13696,.T.);
#19752=ORIENTED_EDGE('',*,*,#13859,.T.);
#19753=ORIENTED_EDGE('',*,*,#13860,.T.);
#19754=ORIENTED_EDGE('',*,*,#13836,.F.);
#19755=ORIENTED_EDGE('',*,*,#13704,.T.);
#19756=ORIENTED_EDGE('',*,*,#13862,.T.);
#19757=ORIENTED_EDGE('',*,*,#13863,.T.);
#19758=ORIENTED_EDGE('',*,*,#13834,.F.);
#19759=ORIENTED_EDGE('',*,*,#13712,.T.);
#19760=ORIENTED_EDGE('',*,*,#13865,.T.);
#19761=ORIENTED_EDGE('',*,*,#13866,.T.);
#19762=ORIENTED_EDGE('',*,*,#13832,.F.);
#19763=ORIENTED_EDGE('',*,*,#13720,.T.);
#19764=ORIENTED_EDGE('',*,*,#13868,.T.);
#19765=ORIENTED_EDGE('',*,*,#13869,.T.);
#19766=ORIENTED_EDGE('',*,*,#13830,.F.);
#19767=ORIENTED_EDGE('',*,*,#13728,.T.);
#19768=ORIENTED_EDGE('',*,*,#13871,.T.);
#19769=ORIENTED_EDGE('',*,*,#13872,.T.);
#19770=ORIENTED_EDGE('',*,*,#13828,.F.);
#19771=ORIENTED_EDGE('',*,*,#13736,.T.);
#19772=ORIENTED_EDGE('',*,*,#13874,.T.);
#19773=ORIENTED_EDGE('',*,*,#13875,.T.);
#19774=ORIENTED_EDGE('',*,*,#13826,.F.);
#19775=ORIENTED_EDGE('',*,*,#13744,.T.);
#19776=ORIENTED_EDGE('',*,*,#13877,.T.);
#19777=ORIENTED_EDGE('',*,*,#13878,.T.);
#19778=ORIENTED_EDGE('',*,*,#13824,.F.);
#19779=ORIENTED_EDGE('',*,*,#13857,.F.);
#19780=ORIENTED_EDGE('',*,*,#13752,.T.);
#19781=ORIENTED_EDGE('',*,*,#13880,.T.);
#19782=ORIENTED_EDGE('',*,*,#13881,.T.);
#19783=ORIENTED_EDGE('',*,*,#13855,.F.);
#19784=ORIENTED_EDGE('',*,*,#13760,.T.);
#19785=ORIENTED_EDGE('',*,*,#13883,.T.);
#19786=ORIENTED_EDGE('',*,*,#13884,.T.);
#19787=ORIENTED_EDGE('',*,*,#13853,.F.);
#19788=ORIENTED_EDGE('',*,*,#13768,.T.);
#19789=ORIENTED_EDGE('',*,*,#13886,.T.);
#19790=ORIENTED_EDGE('',*,*,#13887,.T.);
#19791=ORIENTED_EDGE('',*,*,#13851,.F.);
#19792=ORIENTED_EDGE('',*,*,#13776,.T.);
#19793=ORIENTED_EDGE('',*,*,#13889,.T.);
#19794=ORIENTED_EDGE('',*,*,#13890,.T.);
#19795=ORIENTED_EDGE('',*,*,#13849,.F.);
#19796=ORIENTED_EDGE('',*,*,#13784,.T.);
#19797=ORIENTED_EDGE('',*,*,#13892,.T.);
#19798=ORIENTED_EDGE('',*,*,#13893,.T.);
#19799=ORIENTED_EDGE('',*,*,#13847,.F.);
#19800=ORIENTED_EDGE('',*,*,#13792,.T.);
#19801=ORIENTED_EDGE('',*,*,#13895,.T.);
#19802=ORIENTED_EDGE('',*,*,#13896,.T.);
#19803=ORIENTED_EDGE('',*,*,#13845,.F.);
#19804=ORIENTED_EDGE('',*,*,#13800,.T.);
#19805=ORIENTED_EDGE('',*,*,#13898,.T.);
#19806=ORIENTED_EDGE('',*,*,#13899,.T.);
#19807=ORIENTED_EDGE('',*,*,#13843,.F.);
#19808=ORIENTED_EDGE('',*,*,#13808,.T.);
#19809=ORIENTED_EDGE('',*,*,#13901,.T.);
#19810=ORIENTED_EDGE('',*,*,#13902,.T.);
#19811=ORIENTED_EDGE('',*,*,#13841,.F.);
#19812=ORIENTED_EDGE('',*,*,#13816,.T.);
#19813=ORIENTED_EDGE('',*,*,#13905,.T.);
#19814=ORIENTED_EDGE('',*,*,#13903,.T.);
#19815=ORIENTED_EDGE('',*,*,#13839,.F.);
#19816=ORIENTED_EDGE('',*,*,#13688,.T.);
#19817=ORIENTED_EDGE('',*,*,#13819,.T.);
#19818=ORIENTED_EDGE('',*,*,#13914,.F.);
#19819=ORIENTED_EDGE('',*,*,#13822,.T.);
#19820=ORIENTED_EDGE('',*,*,#13915,.F.);
#19821=ORIENTED_EDGE('',*,*,#13916,.T.);
#19822=ORIENTED_EDGE('',*,*,#13914,.T.);
#19823=ORIENTED_EDGE('',*,*,#13916,.F.);
#19824=ORIENTED_EDGE('',*,*,#13915,.T.);
#19825=ORIENTED_EDGE('',*,*,#13917,.F.);
#19826=ORIENTED_EDGE('',*,*,#13917,.T.);
#19827=ORIENTED_EDGE('',*,*,#13918,.T.);
#19828=ORIENTED_EDGE('',*,*,#13919,.F.);
#19829=ORIENTED_EDGE('',*,*,#13918,.F.);
#19830=ORIENTED_EDGE('',*,*,#13919,.T.);
#19831=ORIENTED_EDGE('',*,*,#13920,.T.);
#19832=ORIENTED_EDGE('',*,*,#13906,.F.);
#19833=ORIENTED_EDGE('',*,*,#13920,.F.);
#21426=CONICAL_SURFACE('',#24232,1.88899277133291,0.209439510239319);
#21427=CONICAL_SURFACE('',#24269,1.96724457939162,0.20943951023932);
#21428=CONICAL_SURFACE('',#24306,2.06222171593972,1.36135681655558);
#21429=CONICAL_SURFACE('',#24307,1.79401563478481,1.36135681655558);
#21430=CONICAL_SURFACE('',#24314,0.32,0.0347685918560824);
#21431=CONICAL_SURFACE('',#24316,0.32,0.0347685918560824);
#21432=CONICAL_SURFACE('',#24326,0.32,0.0347685918560824);
#21433=CONICAL_SURFACE('',#24328,0.32,0.0347685918560824);
#21434=CONICAL_SURFACE('',#24338,0.32,0.0347685918560824);
#21435=CONICAL_SURFACE('',#24340,0.32,0.0347685918560824);
#21436=CONICAL_SURFACE('',#24350,0.32,0.0347685918560824);
#21437=CONICAL_SURFACE('',#24352,0.32,0.0347685918560824);
#21438=CONICAL_SURFACE('',#24362,0.32,0.0347685918560824);
#21439=CONICAL_SURFACE('',#24364,0.32,0.0347685918560824);
#21440=CONICAL_SURFACE('',#24374,0.32,0.0347685918560824);
#21441=CONICAL_SURFACE('',#24376,0.32,0.0347685918560824);
#21442=CONICAL_SURFACE('',#24386,0.32,0.0347685918560824);
#21443=CONICAL_SURFACE('',#24388,0.32,0.0347685918560824);
#21444=CONICAL_SURFACE('',#24398,0.32,0.0347685918560824);
#21445=CONICAL_SURFACE('',#24400,0.32,0.0347685918560824);
#21446=CONICAL_SURFACE('',#24410,0.32,0.0347685918560824);
#21447=CONICAL_SURFACE('',#24412,0.32,0.0347685918560824);
#21448=CONICAL_SURFACE('',#24422,0.32,0.0347685918560824);
#21449=CONICAL_SURFACE('',#24424,0.32,0.0347685918560824);
#21450=CONICAL_SURFACE('',#24434,0.32,0.0347685918560824);
#21451=CONICAL_SURFACE('',#24436,0.32,0.0347685918560824);
#21452=CONICAL_SURFACE('',#24446,0.32,0.0347685918560824);
#21453=CONICAL_SURFACE('',#24448,0.32,0.0347685918560824);
#21454=CONICAL_SURFACE('',#24458,0.32,0.0347685918560824);
#21455=CONICAL_SURFACE('',#24460,0.32,0.0347685918560824);
#21456=CONICAL_SURFACE('',#24470,0.32,0.0347685918560824);
#21457=CONICAL_SURFACE('',#24472,0.32,0.0347685918560824);
#21458=CONICAL_SURFACE('',#24482,0.32,0.0347685918560824);
#21459=CONICAL_SURFACE('',#24484,0.32,0.0347685918560824);
#21460=CONICAL_SURFACE('',#24494,0.32,0.0347685918560824);
#21461=CONICAL_SURFACE('',#24496,0.32,0.0347685918560824);
#21462=CONICAL_SURFACE('',#24508,0.32,0.0347685918560824);
#21463=CONICAL_SURFACE('',#24509,0.32,0.0347685918560824);
#21464=CONICAL_SURFACE('',#24514,0.32,0.0347685918560824);
#21465=CONICAL_SURFACE('',#24516,1.61107777577792,0.174532925199433);
#21466=CONICAL_SURFACE('',#24538,0.32,0.0347685918560824);
#21467=CONICAL_SURFACE('',#24542,0.32,0.0347685918560824);
#21468=CONICAL_SURFACE('',#24546,0.32,0.0347685918560824);
#21469=CONICAL_SURFACE('',#24550,0.32,0.0347685918560824);
#21470=CONICAL_SURFACE('',#24554,0.32,0.0347685918560824);
#21471=CONICAL_SURFACE('',#24558,0.32,0.0347685918560824);
#21472=CONICAL_SURFACE('',#24562,0.32,0.0347685918560824);
#21473=CONICAL_SURFACE('',#24566,0.32,0.0347685918560824);
#21474=CONICAL_SURFACE('',#24570,0.32,0.0347685918560824);
#21475=CONICAL_SURFACE('',#24574,0.32,0.0347685918560824);
#21476=CONICAL_SURFACE('',#24578,0.32,0.0347685918560824);
#21477=CONICAL_SURFACE('',#24582,0.32,0.0347685918560824);
#21478=CONICAL_SURFACE('',#24586,0.32,0.0347685918560824);
#21479=CONICAL_SURFACE('',#24590,0.32,0.0347685918560824);
#21480=CONICAL_SURFACE('',#24594,0.32,0.0347685918560824);
#21481=CONICAL_SURFACE('',#24596,0.32,0.0347685918560824);
#21482=CONICAL_SURFACE('',#24600,1.28,0.785398163397449);
#21483=CONICAL_SURFACE('',#24605,1.87,0.785398163397449);
#21484=CONICAL_SURFACE('',#24616,1.28,0.785398163397448);
#22379=ADVANCED_FACE('',(#3549,#1758,#1759,#1760,#1761,#1762,#1763,#1764,
#1765,#1766,#1767,#1768,#1769,#1770,#1771,#1772,#1773,#1774),#21426,.F.);
#22380=ADVANCED_FACE('',(#3550,#1775,#1776,#1777,#1778,#1779,#1780,#1781,
#1782,#1783,#1784,#1785,#1786,#1787,#1788,#1789,#1790,#1791),#21427,.T.);
#22381=ADVANCED_FACE('',(#3551),#21428,.T.);
#22382=ADVANCED_FACE('',(#3552),#21429,.F.);
#22383=ADVANCED_FACE('',(#3553),#2158,.T.);
#22384=ADVANCED_FACE('',(#3554),#2159,.T.);
#22385=ADVANCED_FACE('',(#3555),#21430,.T.);
#22386=ADVANCED_FACE('',(#3556),#21431,.T.);
#22387=ADVANCED_FACE('',(#3557),#2160,.T.);
#22388=ADVANCED_FACE('',(#3558),#2161,.T.);
#22389=ADVANCED_FACE('',(#3559),#2162,.T.);
#22390=ADVANCED_FACE('',(#3560),#21432,.T.);
#22391=ADVANCED_FACE('',(#3561),#21433,.T.);
#22392=ADVANCED_FACE('',(#3562),#2163,.T.);
#22393=ADVANCED_FACE('',(#3563),#2164,.T.);
#22394=ADVANCED_FACE('',(#3564),#2165,.T.);
#22395=ADVANCED_FACE('',(#3565),#21434,.T.);
#22396=ADVANCED_FACE('',(#3566),#21435,.T.);
#22397=ADVANCED_FACE('',(#3567),#2166,.T.);
#22398=ADVANCED_FACE('',(#3568),#2167,.T.);
#22399=ADVANCED_FACE('',(#3569),#2168,.T.);
#22400=ADVANCED_FACE('',(#3570),#21436,.T.);
#22401=ADVANCED_FACE('',(#3571),#21437,.T.);
#22402=ADVANCED_FACE('',(#3572),#2169,.T.);
#22403=ADVANCED_FACE('',(#3573),#2170,.T.);
#22404=ADVANCED_FACE('',(#3574),#2171,.T.);
#22405=ADVANCED_FACE('',(#3575),#21438,.T.);
#22406=ADVANCED_FACE('',(#3576),#21439,.T.);
#22407=ADVANCED_FACE('',(#3577),#2172,.T.);
#22408=ADVANCED_FACE('',(#3578),#2173,.T.);
#22409=ADVANCED_FACE('',(#3579),#2174,.T.);
#22410=ADVANCED_FACE('',(#3580),#21440,.T.);
#22411=ADVANCED_FACE('',(#3581),#21441,.T.);
#22412=ADVANCED_FACE('',(#3582),#2175,.T.);
#22413=ADVANCED_FACE('',(#3583),#2176,.T.);
#22414=ADVANCED_FACE('',(#3584),#2177,.T.);
#22415=ADVANCED_FACE('',(#3585),#21442,.T.);
#22416=ADVANCED_FACE('',(#3586),#21443,.T.);
#22417=ADVANCED_FACE('',(#3587),#2178,.T.);
#22418=ADVANCED_FACE('',(#3588),#2179,.T.);
#22419=ADVANCED_FACE('',(#3589),#2180,.T.);
#22420=ADVANCED_FACE('',(#3590),#21444,.T.);
#22421=ADVANCED_FACE('',(#3591),#21445,.T.);
#22422=ADVANCED_FACE('',(#3592),#2181,.T.);
#22423=ADVANCED_FACE('',(#3593),#2182,.T.);
#22424=ADVANCED_FACE('',(#3594),#2183,.T.);
#22425=ADVANCED_FACE('',(#3595),#21446,.T.);
#22426=ADVANCED_FACE('',(#3596),#21447,.T.);
#22427=ADVANCED_FACE('',(#3597),#2184,.T.);
#22428=ADVANCED_FACE('',(#3598),#2185,.T.);
#22429=ADVANCED_FACE('',(#3599),#2186,.T.);
#22430=ADVANCED_FACE('',(#3600),#21448,.T.);
#22431=ADVANCED_FACE('',(#3601),#21449,.T.);
#22432=ADVANCED_FACE('',(#3602),#2187,.T.);
#22433=ADVANCED_FACE('',(#3603),#2188,.T.);
#22434=ADVANCED_FACE('',(#3604),#2189,.T.);
#22435=ADVANCED_FACE('',(#3605),#21450,.T.);
#22436=ADVANCED_FACE('',(#3606),#21451,.T.);
#22437=ADVANCED_FACE('',(#3607),#2190,.T.);
#22438=ADVANCED_FACE('',(#3608),#2191,.T.);
#22439=ADVANCED_FACE('',(#3609),#2192,.T.);
#22440=ADVANCED_FACE('',(#3610),#21452,.T.);
#22441=ADVANCED_FACE('',(#3611),#21453,.T.);
#22442=ADVANCED_FACE('',(#3612),#2193,.T.);
#22443=ADVANCED_FACE('',(#3613),#2194,.T.);
#22444=ADVANCED_FACE('',(#3614),#2195,.T.);
#22445=ADVANCED_FACE('',(#3615),#21454,.T.);
#22446=ADVANCED_FACE('',(#3616),#21455,.T.);
#22447=ADVANCED_FACE('',(#3617),#2196,.T.);
#22448=ADVANCED_FACE('',(#3618),#2197,.T.);
#22449=ADVANCED_FACE('',(#3619),#2198,.T.);
#22450=ADVANCED_FACE('',(#3620),#21456,.T.);
#22451=ADVANCED_FACE('',(#3621),#21457,.T.);
#22452=ADVANCED_FACE('',(#3622),#2199,.T.);
#22453=ADVANCED_FACE('',(#3623),#2200,.T.);
#22454=ADVANCED_FACE('',(#3624),#2201,.T.);
#22455=ADVANCED_FACE('',(#3625),#21458,.T.);
#22456=ADVANCED_FACE('',(#3626),#21459,.T.);
#22457=ADVANCED_FACE('',(#3627),#2202,.T.);
#22458=ADVANCED_FACE('',(#3628),#2203,.T.);
#22459=ADVANCED_FACE('',(#3629),#2204,.T.);
#22460=ADVANCED_FACE('',(#3630),#21460,.T.);
#22461=ADVANCED_FACE('',(#3631),#21461,.T.);
#22462=ADVANCED_FACE('',(#3632),#2205,.T.);
#22463=ADVANCED_FACE('',(#3633),#2206,.T.);
#22464=ADVANCED_FACE('',(#3634),#2207,.T.);
#22465=ADVANCED_FACE('',(#3635),#2208,.T.);
#22466=ADVANCED_FACE('',(#3636),#21462,.T.);
#22467=ADVANCED_FACE('',(#3637),#21463,.T.);
#22468=ADVANCED_FACE('',(#3638),#2209,.T.);
#22469=ADVANCED_FACE('',(#3639),#21464,.T.);
#22470=ADVANCED_FACE('',(#3640),#21465,.T.);
#22471=ADVANCED_FACE('',(#3641),#2210,.T.);
#22472=ADVANCED_FACE('',(#3642),#21466,.T.);
#22473=ADVANCED_FACE('',(#3643),#2211,.T.);
#22474=ADVANCED_FACE('',(#3644),#21467,.T.);
#22475=ADVANCED_FACE('',(#3645),#2212,.T.);
#22476=ADVANCED_FACE('',(#3646),#21468,.T.);
#22477=ADVANCED_FACE('',(#3647),#2213,.T.);
#22478=ADVANCED_FACE('',(#3648),#21469,.T.);
#22479=ADVANCED_FACE('',(#3649),#2214,.T.);
#22480=ADVANCED_FACE('',(#3650),#21470,.T.);
#22481=ADVANCED_FACE('',(#3651),#2215,.T.);
#22482=ADVANCED_FACE('',(#3652),#21471,.T.);
#22483=ADVANCED_FACE('',(#3653),#2216,.T.);
#22484=ADVANCED_FACE('',(#3654),#21472,.T.);
#22485=ADVANCED_FACE('',(#3655),#2217,.T.);
#22486=ADVANCED_FACE('',(#3656),#21473,.T.);
#22487=ADVANCED_FACE('',(#3657),#2218,.T.);
#22488=ADVANCED_FACE('',(#3658),#21474,.T.);
#22489=ADVANCED_FACE('',(#3659),#2219,.T.);
#22490=ADVANCED_FACE('',(#3660),#21475,.T.);
#22491=ADVANCED_FACE('',(#3661),#2220,.T.);
#22492=ADVANCED_FACE('',(#3662),#21476,.T.);
#22493=ADVANCED_FACE('',(#3663),#2221,.T.);
#22494=ADVANCED_FACE('',(#3664),#21477,.T.);
#22495=ADVANCED_FACE('',(#3665),#2222,.T.);
#22496=ADVANCED_FACE('',(#3666),#21478,.T.);
#22497=ADVANCED_FACE('',(#3667),#2223,.T.);
#22498=ADVANCED_FACE('',(#3668),#21479,.T.);
#22499=ADVANCED_FACE('',(#3669),#2224,.T.);
#22500=ADVANCED_FACE('',(#3670),#21480,.T.);
#22501=ADVANCED_FACE('',(#3671),#21481,.T.);
#22502=ADVANCED_FACE('',(#3672),#2225,.T.);
#22503=ADVANCED_FACE('',(#3673),#21482,.F.);
#22504=ADVANCED_FACE('',(#3674,#1792),#2226,.T.);
#22505=ADVANCED_FACE('',(#3675),#21483,.T.);
#22506=ADVANCED_FACE('',(#3676),#2579,.T.);
#22507=ADVANCED_FACE('',(#3677,#1793),#2227,.T.);
#22508=ADVANCED_FACE('',(#3678,#1794),#2228,.T.);
#22509=ADVANCED_FACE('',(#3679),#2580,.T.);
#22510=ADVANCED_FACE('',(#3680,#1795),#2229,.T.);
#22511=ADVANCED_FACE('',(#3681),#21484,.F.);
#22512=ADVANCED_FACE('',(#3682),#2581,.F.);
#22819=CLOSED_SHELL('',(#22379,#22380,#22381,#22382,#22383,#22384,#22385,
#22386,#22387,#22388,#22389,#22390,#22391,#22392,#22393,#22394,#22395,#22396,
#22397,#22398,#22399,#22400,#22401,#22402,#22403,#22404,#22405,#22406,#22407,
#22408,#22409,#22410,#22411,#22412,#22413,#22414,#22415,#22416,#22417,#22418,
#22419,#22420,#22421,#22422,#22423,#22424,#22425,#22426,#22427,#22428,#22429,
#22430,#22431,#22432,#22433,#22434,#22435,#22436,#22437,#22438,#22439,#22440,
#22441,#22442,#22443,#22444,#22445,#22446,#22447,#22448,#22449,#22450,#22451,
#22452,#22453,#22454,#22455,#22456,#22457,#22458,#22459,#22460,#22461,#22462,
#22463,#22464,#22465,#22466,#22467,#22468,#22469,#22470,#22471,#22472,#22473,
#22474,#22475,#22476,#22477,#22478,#22479,#22480,#22481,#22482,#22483,#22484,
#22485,#22486,#22487,#22488,#22489,#22490,#22491,#22492,#22493,#22494,#22495,
#22496,#22497,#22498,#22499,#22500,#22501,#22502,#22503,#22504,#22505,#22506,
#22507,#22508,#22509,#22510,#22511,#22512));
#24231=AXIS2_PLACEMENT_3D('',#47402,#28508,#28509);
#24232=AXIS2_PLACEMENT_3D('',#47403,#28510,#28511);
#24233=AXIS2_PLACEMENT_3D('',#47405,#28512,#28513);
#24234=AXIS2_PLACEMENT_3D('',#47408,#28515,#28516);
#24235=AXIS2_PLACEMENT_3D('',#47411,#28517,#28518);
#24236=AXIS2_PLACEMENT_3D('',#47418,#28519,#28520);
#24237=AXIS2_PLACEMENT_3D('',#47425,#28521,#28522);
#24238=AXIS2_PLACEMENT_3D('',#47432,#28523,#28524);
#24239=AXIS2_PLACEMENT_3D('',#47439,#28525,#28526);
#24240=AXIS2_PLACEMENT_3D('',#47446,#28527,#28528);
#24241=AXIS2_PLACEMENT_3D('',#47453,#28529,#28530);
#24242=AXIS2_PLACEMENT_3D('',#47460,#28531,#28532);
#24243=AXIS2_PLACEMENT_3D('',#47467,#28533,#28534);
#24244=AXIS2_PLACEMENT_3D('',#47474,#28535,#28536);
#24245=AXIS2_PLACEMENT_3D('',#47481,#28537,#28538);
#24246=AXIS2_PLACEMENT_3D('',#47488,#28539,#28540);
#24247=AXIS2_PLACEMENT_3D('',#47495,#28541,#28542);
#24248=AXIS2_PLACEMENT_3D('',#47502,#28543,#28544);
#24249=AXIS2_PLACEMENT_3D('',#47509,#28545,#28546);
#24250=AXIS2_PLACEMENT_3D('',#47516,#28547,#28548);
#24251=AXIS2_PLACEMENT_3D('',#47523,#28549,#28550);
#24252=AXIS2_PLACEMENT_3D('',#47530,#28551,#28552);
#24253=AXIS2_PLACEMENT_3D('',#47537,#28553,#28554);
#24254=AXIS2_PLACEMENT_3D('',#47544,#28555,#28556);
#24255=AXIS2_PLACEMENT_3D('',#47551,#28557,#28558);
#24256=AXIS2_PLACEMENT_3D('',#47558,#28559,#28560);
#24257=AXIS2_PLACEMENT_3D('',#47565,#28561,#28562);
#24258=AXIS2_PLACEMENT_3D('',#47572,#28563,#28564);
#24259=AXIS2_PLACEMENT_3D('',#47579,#28565,#28566);
#24260=AXIS2_PLACEMENT_3D('',#47586,#28567,#28568);
#24261=AXIS2_PLACEMENT_3D('',#47593,#28569,#28570);
#24262=AXIS2_PLACEMENT_3D('',#47600,#28571,#28572);
#24263=AXIS2_PLACEMENT_3D('',#47607,#28573,#28574);
#24264=AXIS2_PLACEMENT_3D('',#47614,#28575,#28576);
#24265=AXIS2_PLACEMENT_3D('',#47621,#28577,#28578);
#24266=AXIS2_PLACEMENT_3D('',#47628,#28579,#28580);
#24267=AXIS2_PLACEMENT_3D('',#47640,#28581,#28582);
#24268=AXIS2_PLACEMENT_3D('',#47646,#28583,#28584);
#24269=AXIS2_PLACEMENT_3D('',#47647,#28585,#28586);
#24270=AXIS2_PLACEMENT_3D('',#47649,#28587,#28588);
#24271=AXIS2_PLACEMENT_3D('',#47652,#28590,#28591);
#24272=AXIS2_PLACEMENT_3D('',#47655,#28592,#28593);
#24273=AXIS2_PLACEMENT_3D('',#47662,#28594,#28595);
#24274=AXIS2_PLACEMENT_3D('',#47669,#28596,#28597);
#24275=AXIS2_PLACEMENT_3D('',#47676,#28598,#28599);
#24276=AXIS2_PLACEMENT_3D('',#47683,#28600,#28601);
#24277=AXIS2_PLACEMENT_3D('',#47690,#28602,#28603);
#24278=AXIS2_PLACEMENT_3D('',#47697,#28604,#28605);
#24279=AXIS2_PLACEMENT_3D('',#47704,#28606,#28607);
#24280=AXIS2_PLACEMENT_3D('',#47711,#28608,#28609);
#24281=AXIS2_PLACEMENT_3D('',#47718,#28610,#28611);
#24282=AXIS2_PLACEMENT_3D('',#47725,#28612,#28613);
#24283=AXIS2_PLACEMENT_3D('',#47732,#28614,#28615);
#24284=AXIS2_PLACEMENT_3D('',#47739,#28616,#28617);
#24285=AXIS2_PLACEMENT_3D('',#47746,#28618,#28619);
#24286=AXIS2_PLACEMENT_3D('',#47753,#28620,#28621);
#24287=AXIS2_PLACEMENT_3D('',#47760,#28622,#28623);
#24288=AXIS2_PLACEMENT_3D('',#47767,#28624,#28625);
#24289=AXIS2_PLACEMENT_3D('',#47774,#28626,#28627);
#24290=AXIS2_PLACEMENT_3D('',#47781,#28628,#28629);
#24291=AXIS2_PLACEMENT_3D('',#47788,#28630,#28631);
#24292=AXIS2_PLACEMENT_3D('',#47795,#28632,#28633);
#24293=AXIS2_PLACEMENT_3D('',#47802,#28634,#28635);
#24294=AXIS2_PLACEMENT_3D('',#47809,#28636,#28637);
#24295=AXIS2_PLACEMENT_3D('',#47816,#28638,#28639);
#24296=AXIS2_PLACEMENT_3D('',#47823,#28640,#28641);
#24297=AXIS2_PLACEMENT_3D('',#47830,#28642,#28643);
#24298=AXIS2_PLACEMENT_3D('',#47837,#28644,#28645);
#24299=AXIS2_PLACEMENT_3D('',#47844,#28646,#28647);
#24300=AXIS2_PLACEMENT_3D('',#47851,#28648,#28649);
#24301=AXIS2_PLACEMENT_3D('',#47858,#28650,#28651);
#24302=AXIS2_PLACEMENT_3D('',#47865,#28652,#28653);
#24303=AXIS2_PLACEMENT_3D('',#47872,#28654,#28655);
#24304=AXIS2_PLACEMENT_3D('',#47884,#28656,#28657);
#24305=AXIS2_PLACEMENT_3D('',#47890,#28658,#28659);
#24306=AXIS2_PLACEMENT_3D('',#47891,#28660,#28661);
#24307=AXIS2_PLACEMENT_3D('',#47893,#28663,#28664);
#24308=AXIS2_PLACEMENT_3D('',#47895,#28666,#28667);
#24309=AXIS2_PLACEMENT_3D('',#47896,#28668,#28669);
#24310=AXIS2_PLACEMENT_3D('',#47897,#28670,#28671);
#24311=AXIS2_PLACEMENT_3D('',#47899,#28672,#28673);
#24312=AXIS2_PLACEMENT_3D('',#47901,#28674,#28675);
#24313=AXIS2_PLACEMENT_3D('',#47902,#28676,#28677);
#24314=AXIS2_PLACEMENT_3D('',#47903,#28678,#28679);
#24315=AXIS2_PLACEMENT_3D('',#47904,#28680,#28681);
#24316=AXIS2_PLACEMENT_3D('',#47905,#28682,#28683);
#24317=AXIS2_PLACEMENT_3D('',#47907,#28684,#28685);
#24318=AXIS2_PLACEMENT_3D('',#47909,#28686,#28687);
#24319=AXIS2_PLACEMENT_3D('',#47914,#28688,#28689);
#24320=AXIS2_PLACEMENT_3D('',#47915,#28690,#28691);
#24321=AXIS2_PLACEMENT_3D('',#47916,#28692,#28693);
#24322=AXIS2_PLACEMENT_3D('',#47917,#28694,#28695);
#24323=AXIS2_PLACEMENT_3D('',#47919,#28696,#28697);
#24324=AXIS2_PLACEMENT_3D('',#47921,#28698,#28699);
#24325=AXIS2_PLACEMENT_3D('',#47922,#28700,#28701);
#24326=AXIS2_PLACEMENT_3D('',#47923,#28702,#28703);
#24327=AXIS2_PLACEMENT_3D('',#47924,#28704,#28705);
#24328=AXIS2_PLACEMENT_3D('',#47925,#28706,#28707);
#24329=AXIS2_PLACEMENT_3D('',#47927,#28708,#28709);
#24330=AXIS2_PLACEMENT_3D('',#47929,#28710,#28711);
#24331=AXIS2_PLACEMENT_3D('',#47934,#28712,#28713);
#24332=AXIS2_PLACEMENT_3D('',#47935,#28714,#28715);
#24333=AXIS2_PLACEMENT_3D('',#47936,#28716,#28717);
#24334=AXIS2_PLACEMENT_3D('',#47937,#28718,#28719);
#24335=AXIS2_PLACEMENT_3D('',#47939,#28720,#28721);
#24336=AXIS2_PLACEMENT_3D('',#47941,#28722,#28723);
#24337=AXIS2_PLACEMENT_3D('',#47942,#28724,#28725);
#24338=AXIS2_PLACEMENT_3D('',#47943,#28726,#28727);
#24339=AXIS2_PLACEMENT_3D('',#47944,#28728,#28729);
#24340=AXIS2_PLACEMENT_3D('',#47945,#28730,#28731);
#24341=AXIS2_PLACEMENT_3D('',#47947,#28732,#28733);
#24342=AXIS2_PLACEMENT_3D('',#47949,#28734,#28735);
#24343=AXIS2_PLACEMENT_3D('',#47954,#28736,#28737);
#24344=AXIS2_PLACEMENT_3D('',#47955,#28738,#28739);
#24345=AXIS2_PLACEMENT_3D('',#47956,#28740,#28741);
#24346=AXIS2_PLACEMENT_3D('',#47957,#28742,#28743);
#24347=AXIS2_PLACEMENT_3D('',#47959,#28744,#28745);
#24348=AXIS2_PLACEMENT_3D('',#47961,#28746,#28747);
#24349=AXIS2_PLACEMENT_3D('',#47962,#28748,#28749);
#24350=AXIS2_PLACEMENT_3D('',#47963,#28750,#28751);
#24351=AXIS2_PLACEMENT_3D('',#47964,#28752,#28753);
#24352=AXIS2_PLACEMENT_3D('',#47965,#28754,#28755);
#24353=AXIS2_PLACEMENT_3D('',#47967,#28756,#28757);
#24354=AXIS2_PLACEMENT_3D('',#47969,#28758,#28759);
#24355=AXIS2_PLACEMENT_3D('',#47974,#28760,#28761);
#24356=AXIS2_PLACEMENT_3D('',#47975,#28762,#28763);
#24357=AXIS2_PLACEMENT_3D('',#47976,#28764,#28765);
#24358=AXIS2_PLACEMENT_3D('',#47977,#28766,#28767);
#24359=AXIS2_PLACEMENT_3D('',#47979,#28768,#28769);
#24360=AXIS2_PLACEMENT_3D('',#47981,#28770,#28771);
#24361=AXIS2_PLACEMENT_3D('',#47982,#28772,#28773);
#24362=AXIS2_PLACEMENT_3D('',#47983,#28774,#28775);
#24363=AXIS2_PLACEMENT_3D('',#47984,#28776,#28777);
#24364=AXIS2_PLACEMENT_3D('',#47985,#28778,#28779);
#24365=AXIS2_PLACEMENT_3D('',#47987,#28780,#28781);
#24366=AXIS2_PLACEMENT_3D('',#47989,#28782,#28783);
#24367=AXIS2_PLACEMENT_3D('',#47994,#28784,#28785);
#24368=AXIS2_PLACEMENT_3D('',#47995,#28786,#28787);
#24369=AXIS2_PLACEMENT_3D('',#47996,#28788,#28789);
#24370=AXIS2_PLACEMENT_3D('',#47997,#28790,#28791);
#24371=AXIS2_PLACEMENT_3D('',#47999,#28792,#28793);
#24372=AXIS2_PLACEMENT_3D('',#48001,#28794,#28795);
#24373=AXIS2_PLACEMENT_3D('',#48002,#28796,#28797);
#24374=AXIS2_PLACEMENT_3D('',#48003,#28798,#28799);
#24375=AXIS2_PLACEMENT_3D('',#48004,#28800,#28801);
#24376=AXIS2_PLACEMENT_3D('',#48005,#28802,#28803);
#24377=AXIS2_PLACEMENT_3D('',#48007,#28804,#28805);
#24378=AXIS2_PLACEMENT_3D('',#48009,#28806,#28807);
#24379=AXIS2_PLACEMENT_3D('',#48014,#28808,#28809);
#24380=AXIS2_PLACEMENT_3D('',#48015,#28810,#28811);
#24381=AXIS2_PLACEMENT_3D('',#48016,#28812,#28813);
#24382=AXIS2_PLACEMENT_3D('',#48017,#28814,#28815);
#24383=AXIS2_PLACEMENT_3D('',#48019,#28816,#28817);
#24384=AXIS2_PLACEMENT_3D('',#48021,#28818,#28819);
#24385=AXIS2_PLACEMENT_3D('',#48022,#28820,#28821);
#24386=AXIS2_PLACEMENT_3D('',#48023,#28822,#28823);
#24387=AXIS2_PLACEMENT_3D('',#48024,#28824,#28825);
#24388=AXIS2_PLACEMENT_3D('',#48025,#28826,#28827);
#24389=AXIS2_PLACEMENT_3D('',#48027,#28828,#28829);
#24390=AXIS2_PLACEMENT_3D('',#48029,#28830,#28831);
#24391=AXIS2_PLACEMENT_3D('',#48034,#28832,#28833);
#24392=AXIS2_PLACEMENT_3D('',#48035,#28834,#28835);
#24393=AXIS2_PLACEMENT_3D('',#48036,#28836,#28837);
#24394=AXIS2_PLACEMENT_3D('',#48037,#28838,#28839);
#24395=AXIS2_PLACEMENT_3D('',#48039,#28840,#28841);
#24396=AXIS2_PLACEMENT_3D('',#48041,#28842,#28843);
#24397=AXIS2_PLACEMENT_3D('',#48042,#28844,#28845);
#24398=AXIS2_PLACEMENT_3D('',#48043,#28846,#28847);
#24399=AXIS2_PLACEMENT_3D('',#48044,#28848,#28849);
#24400=AXIS2_PLACEMENT_3D('',#48045,#28850,#28851);
#24401=AXIS2_PLACEMENT_3D('',#48047,#28852,#28853);
#24402=AXIS2_PLACEMENT_3D('',#48049,#28854,#28855);
#24403=AXIS2_PLACEMENT_3D('',#48054,#28856,#28857);
#24404=AXIS2_PLACEMENT_3D('',#48055,#28858,#28859);
#24405=AXIS2_PLACEMENT_3D('',#48056,#28860,#28861);
#24406=AXIS2_PLACEMENT_3D('',#48057,#28862,#28863);
#24407=AXIS2_PLACEMENT_3D('',#48059,#28864,#28865);
#24408=AXIS2_PLACEMENT_3D('',#48061,#28866,#28867);
#24409=AXIS2_PLACEMENT_3D('',#48062,#28868,#28869);
#24410=AXIS2_PLACEMENT_3D('',#48063,#28870,#28871);
#24411=AXIS2_PLACEMENT_3D('',#48064,#28872,#28873);
#24412=AXIS2_PLACEMENT_3D('',#48065,#28874,#28875);
#24413=AXIS2_PLACEMENT_3D('',#48067,#28876,#28877);
#24414=AXIS2_PLACEMENT_3D('',#48069,#28878,#28879);
#24415=AXIS2_PLACEMENT_3D('',#48074,#28880,#28881);
#24416=AXIS2_PLACEMENT_3D('',#48075,#28882,#28883);
#24417=AXIS2_PLACEMENT_3D('',#48076,#28884,#28885);
#24418=AXIS2_PLACEMENT_3D('',#48077,#28886,#28887);
#24419=AXIS2_PLACEMENT_3D('',#48079,#28888,#28889);
#24420=AXIS2_PLACEMENT_3D('',#48081,#28890,#28891);
#24421=AXIS2_PLACEMENT_3D('',#48082,#28892,#28893);
#24422=AXIS2_PLACEMENT_3D('',#48083,#28894,#28895);
#24423=AXIS2_PLACEMENT_3D('',#48084,#28896,#28897);
#24424=AXIS2_PLACEMENT_3D('',#48085,#28898,#28899);
#24425=AXIS2_PLACEMENT_3D('',#48087,#28900,#28901);
#24426=AXIS2_PLACEMENT_3D('',#48089,#28902,#28903);
#24427=AXIS2_PLACEMENT_3D('',#48094,#28904,#28905);
#24428=AXIS2_PLACEMENT_3D('',#48095,#28906,#28907);
#24429=AXIS2_PLACEMENT_3D('',#48096,#28908,#28909);
#24430=AXIS2_PLACEMENT_3D('',#48097,#28910,#28911);
#24431=AXIS2_PLACEMENT_3D('',#48099,#28912,#28913);
#24432=AXIS2_PLACEMENT_3D('',#48101,#28914,#28915);
#24433=AXIS2_PLACEMENT_3D('',#48102,#28916,#28917);
#24434=AXIS2_PLACEMENT_3D('',#48103,#28918,#28919);
#24435=AXIS2_PLACEMENT_3D('',#48104,#28920,#28921);
#24436=AXIS2_PLACEMENT_3D('',#48105,#28922,#28923);
#24437=AXIS2_PLACEMENT_3D('',#48107,#28924,#28925);
#24438=AXIS2_PLACEMENT_3D('',#48109,#28926,#28927);
#24439=AXIS2_PLACEMENT_3D('',#48114,#28928,#28929);
#24440=AXIS2_PLACEMENT_3D('',#48115,#28930,#28931);
#24441=AXIS2_PLACEMENT_3D('',#48116,#28932,#28933);
#24442=AXIS2_PLACEMENT_3D('',#48117,#28934,#28935);
#24443=AXIS2_PLACEMENT_3D('',#48119,#28936,#28937);
#24444=AXIS2_PLACEMENT_3D('',#48121,#28938,#28939);
#24445=AXIS2_PLACEMENT_3D('',#48122,#28940,#28941);
#24446=AXIS2_PLACEMENT_3D('',#48123,#28942,#28943);
#24447=AXIS2_PLACEMENT_3D('',#48124,#28944,#28945);
#24448=AXIS2_PLACEMENT_3D('',#48125,#28946,#28947);
#24449=AXIS2_PLACEMENT_3D('',#48127,#28948,#28949);
#24450=AXIS2_PLACEMENT_3D('',#48129,#28950,#28951);
#24451=AXIS2_PLACEMENT_3D('',#48134,#28952,#28953);
#24452=AXIS2_PLACEMENT_3D('',#48135,#28954,#28955);
#24453=AXIS2_PLACEMENT_3D('',#48136,#28956,#28957);
#24454=AXIS2_PLACEMENT_3D('',#48137,#28958,#28959);
#24455=AXIS2_PLACEMENT_3D('',#48139,#28960,#28961);
#24456=AXIS2_PLACEMENT_3D('',#48141,#28962,#28963);
#24457=AXIS2_PLACEMENT_3D('',#48142,#28964,#28965);
#24458=AXIS2_PLACEMENT_3D('',#48143,#28966,#28967);
#24459=AXIS2_PLACEMENT_3D('',#48144,#28968,#28969);
#24460=AXIS2_PLACEMENT_3D('',#48145,#28970,#28971);
#24461=AXIS2_PLACEMENT_3D('',#48147,#28972,#28973);
#24462=AXIS2_PLACEMENT_3D('',#48149,#28974,#28975);
#24463=AXIS2_PLACEMENT_3D('',#48154,#28976,#28977);
#24464=AXIS2_PLACEMENT_3D('',#48155,#28978,#28979);
#24465=AXIS2_PLACEMENT_3D('',#48156,#28980,#28981);
#24466=AXIS2_PLACEMENT_3D('',#48157,#28982,#28983);
#24467=AXIS2_PLACEMENT_3D('',#48159,#28984,#28985);
#24468=AXIS2_PLACEMENT_3D('',#48161,#28986,#28987);
#24469=AXIS2_PLACEMENT_3D('',#48162,#28988,#28989);
#24470=AXIS2_PLACEMENT_3D('',#48163,#28990,#28991);
#24471=AXIS2_PLACEMENT_3D('',#48164,#28992,#28993);
#24472=AXIS2_PLACEMENT_3D('',#48165,#28994,#28995);
#24473=AXIS2_PLACEMENT_3D('',#48167,#28996,#28997);
#24474=AXIS2_PLACEMENT_3D('',#48169,#28998,#28999);
#24475=AXIS2_PLACEMENT_3D('',#48174,#29000,#29001);
#24476=AXIS2_PLACEMENT_3D('',#48175,#29002,#29003);
#24477=AXIS2_PLACEMENT_3D('',#48176,#29004,#29005);
#24478=AXIS2_PLACEMENT_3D('',#48177,#29006,#29007);
#24479=AXIS2_PLACEMENT_3D('',#48179,#29008,#29009);
#24480=AXIS2_PLACEMENT_3D('',#48181,#29010,#29011);
#24481=AXIS2_PLACEMENT_3D('',#48182,#29012,#29013);
#24482=AXIS2_PLACEMENT_3D('',#48183,#29014,#29015);
#24483=AXIS2_PLACEMENT_3D('',#48184,#29016,#29017);
#24484=AXIS2_PLACEMENT_3D('',#48185,#29018,#29019);
#24485=AXIS2_PLACEMENT_3D('',#48187,#29020,#29021);
#24486=AXIS2_PLACEMENT_3D('',#48189,#29022,#29023);
#24487=AXIS2_PLACEMENT_3D('',#48194,#29024,#29025);
#24488=AXIS2_PLACEMENT_3D('',#48195,#29026,#29027);
#24489=AXIS2_PLACEMENT_3D('',#48196,#29028,#29029);
#24490=AXIS2_PLACEMENT_3D('',#48197,#29030,#29031);
#24491=AXIS2_PLACEMENT_3D('',#48199,#29032,#29033);
#24492=AXIS2_PLACEMENT_3D('',#48201,#29034,#29035);
#24493=AXIS2_PLACEMENT_3D('',#48202,#29036,#29037);
#24494=AXIS2_PLACEMENT_3D('',#48203,#29038,#29039);
#24495=AXIS2_PLACEMENT_3D('',#48204,#29040,#29041);
#24496=AXIS2_PLACEMENT_3D('',#48205,#29042,#29043);
#24497=AXIS2_PLACEMENT_3D('',#48207,#29044,#29045);
#24498=AXIS2_PLACEMENT_3D('',#48209,#29046,#29047);
#24499=AXIS2_PLACEMENT_3D('',#48214,#29048,#29049);
#24500=AXIS2_PLACEMENT_3D('',#48215,#29050,#29051);
#24501=AXIS2_PLACEMENT_3D('',#48216,#29052,#29053);
#24502=AXIS2_PLACEMENT_3D('',#48217,#29054,#29055);
#24503=AXIS2_PLACEMENT_3D('',#48218,#29056,#29057);
#24504=AXIS2_PLACEMENT_3D('',#48219,#29058,#29059);
#24505=AXIS2_PLACEMENT_3D('',#48221,#29060,#29061);
#24506=AXIS2_PLACEMENT_3D('',#48223,#29062,#29063);
#24507=AXIS2_PLACEMENT_3D('',#48224,#29064,#29065);
#24508=AXIS2_PLACEMENT_3D('',#48225,#29066,#29067);
#24509=AXIS2_PLACEMENT_3D('',#48226,#29068,#29069);
#24510=AXIS2_PLACEMENT_3D('',#48228,#29070,#29071);
#24511=AXIS2_PLACEMENT_3D('',#48230,#29072,#29073);
#24512=AXIS2_PLACEMENT_3D('',#48235,#29074,#29075);
#24513=AXIS2_PLACEMENT_3D('',#48237,#29076,#29077);
#24514=AXIS2_PLACEMENT_3D('',#48239,#29079,#29080);
#24515=AXIS2_PLACEMENT_3D('',#48245,#29081,#29082);
#24516=AXIS2_PLACEMENT_3D('',#48246,#29083,#29084);
#24517=AXIS2_PLACEMENT_3D('',#48248,#29085,#29086);
#24518=AXIS2_PLACEMENT_3D('',#48252,#29088,#29089);
#24519=AXIS2_PLACEMENT_3D('',#48258,#29090,#29091);
#24520=AXIS2_PLACEMENT_3D('',#48264,#29092,#29093);
#24521=AXIS2_PLACEMENT_3D('',#48270,#29094,#29095);
#24522=AXIS2_PLACEMENT_3D('',#48276,#29096,#29097);
#24523=AXIS2_PLACEMENT_3D('',#48282,#29098,#29099);
#24524=AXIS2_PLACEMENT_3D('',#48288,#29100,#29101);
#24525=AXIS2_PLACEMENT_3D('',#48293,#29102,#29103);
#24526=AXIS2_PLACEMENT_3D('',#48295,#29104,#29105);
#24527=AXIS2_PLACEMENT_3D('',#48301,#29106,#29107);
#24528=AXIS2_PLACEMENT_3D('',#48307,#29108,#29109);
#24529=AXIS2_PLACEMENT_3D('',#48313,#29110,#29111);
#24530=AXIS2_PLACEMENT_3D('',#48319,#29112,#29113);
#24531=AXIS2_PLACEMENT_3D('',#48325,#29114,#29115);
#24532=AXIS2_PLACEMENT_3D('',#48331,#29116,#29117);
#24533=AXIS2_PLACEMENT_3D('',#48337,#29118,#29119);
#24534=AXIS2_PLACEMENT_3D('',#48343,#29120,#29121);
#24535=AXIS2_PLACEMENT_3D('',#48348,#29122,#29123);
#24536=AXIS2_PLACEMENT_3D('',#48349,#29124,#29125);
#24537=AXIS2_PLACEMENT_3D('',#48351,#29126,#29127);
#24538=AXIS2_PLACEMENT_3D('',#48353,#29129,#29130);
#24539=AXIS2_PLACEMENT_3D('',#48354,#29131,#29132);
#24540=AXIS2_PLACEMENT_3D('',#48355,#29133,#29134);
#24541=AXIS2_PLACEMENT_3D('',#48357,#29135,#29136);
#24542=AXIS2_PLACEMENT_3D('',#48359,#29138,#29139);
#24543=AXIS2_PLACEMENT_3D('',#48360,#29140,#29141);
#24544=AXIS2_PLACEMENT_3D('',#48361,#29142,#29143);
#24545=AXIS2_PLACEMENT_3D('',#48363,#29144,#29145);
#24546=AXIS2_PLACEMENT_3D('',#48365,#29147,#29148);
#24547=AXIS2_PLACEMENT_3D('',#48366,#29149,#29150);
#24548=AXIS2_PLACEMENT_3D('',#48367,#29151,#29152);
#24549=AXIS2_PLACEMENT_3D('',#48369,#29153,#29154);
#24550=AXIS2_PLACEMENT_3D('',#48371,#29156,#29157);
#24551=AXIS2_PLACEMENT_3D('',#48372,#29158,#29159);
#24552=AXIS2_PLACEMENT_3D('',#48373,#29160,#29161);
#24553=AXIS2_PLACEMENT_3D('',#48375,#29162,#29163);
#24554=AXIS2_PLACEMENT_3D('',#48377,#29165,#29166);
#24555=AXIS2_PLACEMENT_3D('',#48378,#29167,#29168);
#24556=AXIS2_PLACEMENT_3D('',#48379,#29169,#29170);
#24557=AXIS2_PLACEMENT_3D('',#48381,#29171,#29172);
#24558=AXIS2_PLACEMENT_3D('',#48383,#29174,#29175);
#24559=AXIS2_PLACEMENT_3D('',#48384,#29176,#29177);
#24560=AXIS2_PLACEMENT_3D('',#48385,#29178,#29179);
#24561=AXIS2_PLACEMENT_3D('',#48387,#29180,#29181);
#24562=AXIS2_PLACEMENT_3D('',#48389,#29183,#29184);
#24563=AXIS2_PLACEMENT_3D('',#48390,#29185,#29186);
#24564=AXIS2_PLACEMENT_3D('',#48391,#29187,#29188);
#24565=AXIS2_PLACEMENT_3D('',#48393,#29189,#29190);
#24566=AXIS2_PLACEMENT_3D('',#48395,#29192,#29193);
#24567=AXIS2_PLACEMENT_3D('',#48396,#29194,#29195);
#24568=AXIS2_PLACEMENT_3D('',#48397,#29196,#29197);
#24569=AXIS2_PLACEMENT_3D('',#48399,#29198,#29199);
#24570=AXIS2_PLACEMENT_3D('',#48401,#29201,#29202);
#24571=AXIS2_PLACEMENT_3D('',#48402,#29203,#29204);
#24572=AXIS2_PLACEMENT_3D('',#48403,#29205,#29206);
#24573=AXIS2_PLACEMENT_3D('',#48405,#29207,#29208);
#24574=AXIS2_PLACEMENT_3D('',#48407,#29210,#29211);
#24575=AXIS2_PLACEMENT_3D('',#48408,#29212,#29213);
#24576=AXIS2_PLACEMENT_3D('',#48409,#29214,#29215);
#24577=AXIS2_PLACEMENT_3D('',#48411,#29216,#29217);
#24578=AXIS2_PLACEMENT_3D('',#48413,#29219,#29220);
#24579=AXIS2_PLACEMENT_3D('',#48414,#29221,#29222);
#24580=AXIS2_PLACEMENT_3D('',#48415,#29223,#29224);
#24581=AXIS2_PLACEMENT_3D('',#48417,#29225,#29226);
#24582=AXIS2_PLACEMENT_3D('',#48419,#29228,#29229);
#24583=AXIS2_PLACEMENT_3D('',#48420,#29230,#29231);
#24584=AXIS2_PLACEMENT_3D('',#48421,#29232,#29233);
#24585=AXIS2_PLACEMENT_3D('',#48423,#29234,#29235);
#24586=AXIS2_PLACEMENT_3D('',#48425,#29237,#29238);
#24587=AXIS2_PLACEMENT_3D('',#48426,#29239,#29240);
#24588=AXIS2_PLACEMENT_3D('',#48427,#29241,#29242);
#24589=AXIS2_PLACEMENT_3D('',#48429,#29243,#29244);
#24590=AXIS2_PLACEMENT_3D('',#48431,#29246,#29247);
#24591=AXIS2_PLACEMENT_3D('',#48432,#29248,#29249);
#24592=AXIS2_PLACEMENT_3D('',#48433,#29250,#29251);
#24593=AXIS2_PLACEMENT_3D('',#48435,#29252,#29253);
#24594=AXIS2_PLACEMENT_3D('',#48437,#29255,#29256);
#24595=AXIS2_PLACEMENT_3D('',#48438,#29257,#29258);
#24596=AXIS2_PLACEMENT_3D('',#48439,#29259,#29260);
#24597=AXIS2_PLACEMENT_3D('',#48441,#29261,#29262);
#24598=AXIS2_PLACEMENT_3D('',#48442,#29263,#29264);
#24599=AXIS2_PLACEMENT_3D('',#48443,#29265,#29266);
#24600=AXIS2_PLACEMENT_3D('',#48445,#29268,#29269);
#24601=AXIS2_PLACEMENT_3D('',#48447,#29270,#29271);
#24602=AXIS2_PLACEMENT_3D('',#48450,#29273,#29274);
#24603=AXIS2_PLACEMENT_3D('',#48451,#29275,#29276);
#24604=AXIS2_PLACEMENT_3D('',#48453,#29277,#29278);
#24605=AXIS2_PLACEMENT_3D('',#48454,#29279,#29280);
#24606=AXIS2_PLACEMENT_3D('',#48456,#29281,#29282);
#24607=AXIS2_PLACEMENT_3D('',#48458,#29284,#29285);
#24608=AXIS2_PLACEMENT_3D('',#48460,#29286,#29287);
#24609=AXIS2_PLACEMENT_3D('',#48462,#29289,#29290);
#24610=AXIS2_PLACEMENT_3D('',#48463,#29291,#29292);
#24611=AXIS2_PLACEMENT_3D('',#48465,#29293,#29294);
#24612=AXIS2_PLACEMENT_3D('',#48466,#29295,#29296);
#24613=AXIS2_PLACEMENT_3D('',#48468,#29297,#29298);
#24614=AXIS2_PLACEMENT_3D('',#48470,#29300,#29301);
#24615=AXIS2_PLACEMENT_3D('',#48472,#29302,#29303);
#24616=AXIS2_PLACEMENT_3D('',#48473,#29304,#29305);
#24617=AXIS2_PLACEMENT_3D('',#48476,#29307,#29308);
#24618=AXIS2_PLACEMENT_3D('',#48477,#29309,#29310);
#28508=DIRECTION('axis',(0.,0.,1.));
#28509=DIRECTION('refdir',(1.,0.,0.));
#28510=DIRECTION('center_axis',(0.,0.,-1.));
#28511=DIRECTION('ref_axis',(1.,0.,0.));
#28512=DIRECTION('center_axis',(0.,0.,1.));
#28513=DIRECTION('ref_axis',(1.,0.,0.));
#28514=DIRECTION('',(-0.207911690817759,-2.54618386665283E-17,-0.978147600733806));
#28515=DIRECTION('center_axis',(0.,0.,1.));
#28516=DIRECTION('ref_axis',(1.,0.,0.));
#28517=DIRECTION('center_axis',(0.193871877856065,-0.0751063656107956,-0.978147600733806));
#28518=DIRECTION('ref_axis',(0.912095473942782,-0.353347669066023,0.207911690817759));
#28519=DIRECTION('center_axis',(-0.193871877856065,0.0751063656107956,0.978147600733806));
#28520=DIRECTION('ref_axis',(0.912095473942777,-0.353347669066036,0.207911690817759));
#28521=DIRECTION('center_axis',(0.153648593508749,-0.140069200367114,-0.978147600733806));
#28522=DIRECTION('ref_axis',(0.72285979930028,-0.658973777457692,0.207911690817759));
#28523=DIRECTION('center_axis',(-0.153648593508749,0.140069200367114,0.978147600733806));
#28524=DIRECTION('ref_axis',(-0.722859799300274,0.658973777457698,-0.207911690817759));
#28525=DIRECTION('center_axis',(0.0926742152118281,-0.186114913463622,-0.978147600733806));
#28526=DIRECTION('ref_axis',(-0.435997903257843,0.875601825703936,-0.207911690817759));
#28527=DIRECTION('center_axis',(-0.0926742152118281,0.186114913463622,0.978147600733806));
#28528=DIRECTION('ref_axis',(-0.435997903257843,0.875601825703936,-0.207911690817759));
#28529=DIRECTION('center_axis',(0.0191836706249958,-0.207024776198529,-0.978147600733806));
#28530=DIRECTION('ref_axis',(0.0902520744326832,-0.973974995511639,0.207911690817759));
#28531=DIRECTION('center_axis',(-0.0191836706249958,0.207024776198529,0.978147600733806));
#28532=DIRECTION('ref_axis',(-0.09025207443267,0.973974995511641,-0.207911690817759));
#28533=DIRECTION('center_axis',(-0.0568977349801305,-0.19997479574394,-0.978147600733806));
#28534=DIRECTION('ref_axis',(-0.267682797148639,-0.940807445193745,0.207911690817759));
#28535=DIRECTION('center_axis',(0.0568977349801305,0.19997479574394,0.978147600733806));
#28536=DIRECTION('ref_axis',(0.267682797148655,0.94080744519374,-0.207911690817759));
#28537=DIRECTION('center_axis',(-0.125294786194957,-0.165917111025535,-0.978147600733806));
#28538=DIRECTION('ref_axis',(0.589465623693464,0.780578636208407,-0.207911690817759));
#28539=DIRECTION('center_axis',(0.125294786194957,0.165917111025535,0.978147600733806));
#28540=DIRECTION('ref_axis',(0.589465623693459,0.78057863620841,-0.207911690817759));
#28541=DIRECTION('center_axis',(-0.176770082251776,-0.109451401084681,-0.978147600733806));
#28542=DIRECTION('ref_axis',(0.831637851416697,0.514928357067584,-0.207911690817759));
#28543=DIRECTION('center_axis',(0.176770082251776,0.109451401084681,0.978147600733806));
#28544=DIRECTION('ref_axis',(-0.831637851416687,-0.514928357067599,0.207911690817759));
#28545=DIRECTION('center_axis',(-0.204371599183654,-0.0382036729361911,
-0.978147600733806));
#28546=DIRECTION('ref_axis',(-0.961492779041678,-0.179734149988288,0.207911690817759));
#28547=DIRECTION('center_axis',(0.204371599183654,0.0382036729361911,0.978147600733806));
#28548=DIRECTION('ref_axis',(-0.961492779041679,-0.179734149988278,0.207911690817759));
#28549=DIRECTION('center_axis',(-0.204371599183654,0.0382036729361911,-0.978147600733806));
#28550=DIRECTION('ref_axis',(-0.961492779041682,0.179734149988266,0.207911690817759));
#28551=DIRECTION('center_axis',(0.204371599183654,-0.0382036729361911,0.978147600733806));
#28552=DIRECTION('ref_axis',(-0.961492779041682,0.179734149988263,0.207911690817759));
#28553=DIRECTION('center_axis',(-0.176770082251776,0.109451401084681,-0.978147600733806));
#28554=DIRECTION('ref_axis',(0.831637851416689,-0.514928357067596,-0.207911690817759));
#28555=DIRECTION('center_axis',(0.176770082251776,-0.109451401084681,0.978147600733806));
#28556=DIRECTION('ref_axis',(0.831637851416683,-0.514928357067606,-0.207911690817759));
#28557=DIRECTION('center_axis',(-0.125294786194957,0.165917111025535,-0.978147600733806));
#28558=DIRECTION('ref_axis',(0.589465623693458,-0.780578636208411,-0.207911690817759));
#28559=DIRECTION('center_axis',(0.125294786194957,-0.165917111025535,0.978147600733806));
#28560=DIRECTION('ref_axis',(-0.589465623693466,0.780578636208405,0.207911690817759));
#28561=DIRECTION('center_axis',(-0.0568977349801304,0.19997479574394,-0.978147600733806));
#28562=DIRECTION('ref_axis',(0.267682797148634,-0.940807445193746,-0.207911690817759));
#28563=DIRECTION('center_axis',(0.0568977349801304,-0.19997479574394,0.978147600733806));
#28564=DIRECTION('ref_axis',(-0.267682797148657,0.94080744519374,0.207911690817759));
#28565=DIRECTION('center_axis',(0.0191836706249959,0.207024776198529,-0.978147600733806));
#28566=DIRECTION('ref_axis',(-0.0902520744327104,-0.973974995511637,-0.207911690817759));
#28567=DIRECTION('center_axis',(-0.0191836706249959,-0.207024776198529,
0.978147600733806));
#28568=DIRECTION('ref_axis',(-0.0902520744326996,-0.973974995511638,-0.207911690817759));
#28569=DIRECTION('center_axis',(0.092674215211828,0.186114913463622,-0.978147600733806));
#28570=DIRECTION('ref_axis',(-0.435997903257874,-0.87560182570392,-0.207911690817759));
#28571=DIRECTION('center_axis',(-0.092674215211828,-0.186114913463622,0.978147600733806));
#28572=DIRECTION('ref_axis',(-0.435997903257872,-0.875601825703921,-0.207911690817759));
#28573=DIRECTION('center_axis',(0.153648593508749,0.140069200367114,-0.978147600733806));
#28574=DIRECTION('ref_axis',(-0.722859799300277,-0.658973777457695,-0.207911690817759));
#28575=DIRECTION('center_axis',(-0.153648593508749,-0.140069200367114,0.978147600733806));
#28576=DIRECTION('ref_axis',(0.722859799300275,0.658973777457698,0.207911690817759));
#28577=DIRECTION('center_axis',(0.193871877856065,0.0751063656107956,-0.978147600733806));
#28578=DIRECTION('ref_axis',(-0.91209547394278,-0.353347669066029,-0.207911690817759));
#28579=DIRECTION('center_axis',(-0.193871877856065,-0.0751063656107956,
0.978147600733806));
#28580=DIRECTION('ref_axis',(-0.912095473942774,-0.353347669066044,-0.207911690817759));
#28581=DIRECTION('center_axis',(-0.207911690817759,0.,0.978147600733806));
#28582=DIRECTION('ref_axis',(-0.978147600733806,1.44941316600844E-14,-0.207911690817759));
#28583=DIRECTION('center_axis',(0.207911690817759,0.,-0.978147600733806));
#28584=DIRECTION('ref_axis',(-0.978147600733806,2.89270309802114E-14,-0.207911690817759));
#28585=DIRECTION('center_axis',(0.,0.,-1.));
#28586=DIRECTION('ref_axis',(1.,0.,0.));
#28587=DIRECTION('center_axis',(0.,0.,1.));
#28588=DIRECTION('ref_axis',(1.,0.,0.));
#28589=DIRECTION('',(-0.207911690817759,-2.54618386665283E-17,-0.978147600733806));
#28590=DIRECTION('center_axis',(0.,0.,1.));
#28591=DIRECTION('ref_axis',(1.,0.,0.));
#28592=DIRECTION('center_axis',(-0.193871877856065,0.0751063656107956,0.978147600733806));
#28593=DIRECTION('ref_axis',(-0.912095473942771,0.353347669066052,-0.207911690817759));
#28594=DIRECTION('center_axis',(0.193871877856065,-0.0751063656107956,-0.978147600733806));
#28595=DIRECTION('ref_axis',(0.912095473942774,-0.353347669066046,0.207911690817759));
#28596=DIRECTION('center_axis',(-0.153648593508749,0.140069200367114,0.978147600733806));
#28597=DIRECTION('ref_axis',(-0.722859799300271,0.658973777457701,-0.207911690817759));
#28598=DIRECTION('center_axis',(0.153648593508749,-0.140069200367114,-0.978147600733806));
#28599=DIRECTION('ref_axis',(-0.722859799300268,0.658973777457704,-0.207911690817759));
#28600=DIRECTION('center_axis',(-0.0926742152118281,0.186114913463622,0.978147600733806));
#28601=DIRECTION('ref_axis',(-0.435997903257849,0.875601825703933,-0.207911690817759));
#28602=DIRECTION('center_axis',(0.0926742152118281,-0.186114913463622,-0.978147600733806));
#28603=DIRECTION('ref_axis',(0.435997903257857,-0.875601825703929,0.207911690817759));
#28604=DIRECTION('center_axis',(-0.0191836706249958,0.207024776198529,0.978147600733806));
#28605=DIRECTION('ref_axis',(-0.0902520744326517,0.973974995511642,-0.20791169081776));
#28606=DIRECTION('center_axis',(0.0191836706249958,-0.207024776198529,-0.978147600733806));
#28607=DIRECTION('ref_axis',(-0.0902520744326596,0.973974995511642,-0.207911690817759));
#28608=DIRECTION('center_axis',(0.0568977349801305,0.19997479574394,0.978147600733806));
#28609=DIRECTION('ref_axis',(-0.267682797148646,-0.940807445193743,0.207911690817759));
#28610=DIRECTION('center_axis',(-0.0568977349801305,-0.19997479574394,-0.978147600733806));
#28611=DIRECTION('ref_axis',(0.267682797148649,0.940807445193742,-0.207911690817759));
#28612=DIRECTION('center_axis',(0.125294786194957,0.165917111025535,0.978147600733806));
#28613=DIRECTION('ref_axis',(-0.589465623693455,-0.780578636208413,0.207911690817759));
#28614=DIRECTION('center_axis',(-0.125294786194957,-0.165917111025535,-0.978147600733806));
#28615=DIRECTION('ref_axis',(-0.589465623693456,-0.780578636208413,0.207911690817759));
#28616=DIRECTION('center_axis',(0.176770082251776,0.109451401084681,0.978147600733806));
#28617=DIRECTION('ref_axis',(-0.831637851416686,-0.514928357067601,0.207911690817759));
#28618=DIRECTION('center_axis',(-0.176770082251776,-0.109451401084681,-0.978147600733806));
#28619=DIRECTION('ref_axis',(-0.831637851416685,-0.514928357067603,0.207911690817759));
#28620=DIRECTION('center_axis',(0.204371599183654,0.0382036729361911,0.978147600733806));
#28621=DIRECTION('ref_axis',(-0.961492779041674,-0.179734149988305,0.207911690817759));
#28622=DIRECTION('center_axis',(-0.204371599183654,-0.0382036729361911,
-0.978147600733806));
#28623=DIRECTION('ref_axis',(-0.96149277904168,-0.179734149988275,0.207911690817759));
#28624=DIRECTION('center_axis',(0.204371599183654,-0.0382036729361911,0.978147600733806));
#28625=DIRECTION('ref_axis',(0.96149277904168,-0.179734149988275,-0.20791169081776));
#28626=DIRECTION('center_axis',(-0.204371599183654,0.0382036729361911,-0.978147600733806));
#28627=DIRECTION('ref_axis',(-0.961492779041682,0.179734149988263,0.207911690817759));
#28628=DIRECTION('center_axis',(0.176770082251776,-0.109451401084681,0.978147600733806));
#28629=DIRECTION('ref_axis',(-0.831637851416696,0.514928357067584,0.207911690817759));
#28630=DIRECTION('center_axis',(-0.176770082251776,0.109451401084681,-0.978147600733806));
#28631=DIRECTION('ref_axis',(-0.831637851416691,0.514928357067592,0.207911690817759));
#28632=DIRECTION('center_axis',(0.125294786194957,-0.165917111025535,0.978147600733806));
#28633=DIRECTION('ref_axis',(0.589465623693455,-0.780578636208414,-0.207911690817759));
#28634=DIRECTION('center_axis',(-0.125294786194957,0.165917111025535,-0.978147600733806));
#28635=DIRECTION('ref_axis',(0.589465623693456,-0.780578636208413,-0.207911690817759));
#28636=DIRECTION('center_axis',(0.0568977349801304,-0.19997479574394,0.978147600733806));
#28637=DIRECTION('ref_axis',(0.267682797148621,-0.94080744519375,-0.207911690817759));
#28638=DIRECTION('center_axis',(-0.0568977349801304,0.19997479574394,-0.978147600733806));
#28639=DIRECTION('ref_axis',(0.267682797148624,-0.940807445193749,-0.207911690817759));
#28640=DIRECTION('center_axis',(-0.0191836706249959,-0.207024776198529,
0.978147600733806));
#28641=DIRECTION('ref_axis',(-0.0902520744327203,-0.973974995511636,-0.207911690817759));
#28642=DIRECTION('center_axis',(0.0191836706249959,0.207024776198529,-0.978147600733806));
#28643=DIRECTION('ref_axis',(-0.0902520744327027,-0.973974995511638,-0.207911690817759));
#28644=DIRECTION('center_axis',(-0.092674215211828,-0.186114913463622,0.978147600733806));
#28645=DIRECTION('ref_axis',(-0.435997903257856,-0.875601825703929,-0.207911690817759));
#28646=DIRECTION('center_axis',(0.092674215211828,0.186114913463622,-0.978147600733806));
#28647=DIRECTION('ref_axis',(0.435997903257841,0.875601825703937,0.207911690817759));
#28648=DIRECTION('center_axis',(-0.153648593508749,-0.140069200367114,0.978147600733806));
#28649=DIRECTION('ref_axis',(-0.722859799300277,-0.658973777457695,-0.207911690817759));
#28650=DIRECTION('center_axis',(0.153648593508749,0.140069200367114,-0.978147600733806));
#28651=DIRECTION('ref_axis',(0.722859799300275,0.658973777457697,0.207911690817759));
#28652=DIRECTION('center_axis',(-0.193871877856065,-0.0751063656107956,
0.978147600733806));
#28653=DIRECTION('ref_axis',(-0.912095473942778,-0.353347669066035,-0.207911690817759));
#28654=DIRECTION('center_axis',(0.193871877856065,0.0751063656107956,-0.978147600733806));
#28655=DIRECTION('ref_axis',(-0.91209547394278,-0.353347669066029,-0.20791169081776));
#28656=DIRECTION('center_axis',(-0.207911690817759,0.,0.978147600733806));
#28657=DIRECTION('ref_axis',(-0.978147600733806,4.72416904338303E-15,-0.207911690817759));
#28658=DIRECTION('center_axis',(0.207911690817759,0.,-0.978147600733806));
#28659=DIRECTION('ref_axis',(-0.978147600733806,1.44941316600844E-14,-0.207911690817759));
#28660=DIRECTION('center_axis',(0.,0.,1.));
#28661=DIRECTION('ref_axis',(1.,0.,0.));
#28662=DIRECTION('',(0.978147600733806,1.19788532833232E-16,-0.207911690817759));
#28663=DIRECTION('center_axis',(0.,0.,1.));
#28664=DIRECTION('ref_axis',(1.,0.,0.));
#28665=DIRECTION('',(0.978147600733805,1.19788532833232E-16,-0.207911690817761));
#28666=DIRECTION('center_axis',(-0.193871877856065,0.0751063656107956,0.978147600733806));
#28667=DIRECTION('ref_axis',(0.912095473942774,-0.353347669066046,0.207911690817759));
#28668=DIRECTION('center_axis',(-0.193871877856065,0.0751063656107956,0.978147600733806));
#28669=DIRECTION('ref_axis',(0.912095473942773,-0.353347669066046,0.207911690817759));
#28670=DIRECTION('center_axis',(-0.193871877856065,0.0751063656107956,0.978147600733806));
#28671=DIRECTION('ref_axis',(0.912095473942774,-0.353347669066046,0.207911690817759));
#28672=DIRECTION('center_axis',(-0.193871877856065,0.0751063656107956,0.978147600733806));
#28673=DIRECTION('ref_axis',(0.912095473942773,-0.353347669066046,0.207911690817759));
#28674=DIRECTION('center_axis',(-0.193871877856065,0.0751063656107956,0.978147600733806));
#28675=DIRECTION('ref_axis',(-0.91209547394277,0.353347669066056,-0.207911690817759));
#28676=DIRECTION('center_axis',(-0.193871877856065,0.0751063656107956,0.978147600733806));
#28677=DIRECTION('ref_axis',(0.912095473942773,-0.353347669066046,0.207911690817759));
#28678=DIRECTION('center_axis',(0.193871877856065,-0.0751063656107956,-0.978147600733806));
#28679=DIRECTION('ref_axis',(0.912095473942773,-0.353347669066046,0.207911690817759));
#28680=DIRECTION('center_axis',(-0.193871877856065,0.0751063656107956,0.978147600733806));
#28681=DIRECTION('ref_axis',(0.912095473942773,-0.353347669066046,0.207911690817759));
#28682=DIRECTION('center_axis',(0.193871877856065,-0.0751063656107956,-0.978147600733806));
#28683=DIRECTION('ref_axis',(0.912095473942773,-0.353347669066046,0.207911690817759));
#28684=DIRECTION('center_axis',(-0.193871877856065,0.0751063656107956,0.978147600733806));
#28685=DIRECTION('ref_axis',(0.912095473942773,-0.353347669066046,0.207911690817759));
#28686=DIRECTION('center_axis',(0.,0.,-1.));
#28687=DIRECTION('ref_axis',(-0.932472229404348,0.361241666187173,1.58735880974294E-16));
#28688=DIRECTION('center_axis',(0.193871877856065,-0.0751063656107956,-0.978147600733806));
#28689=DIRECTION('ref_axis',(-0.912095473942774,0.353347669066046,-0.207911690817759));
#28690=DIRECTION('center_axis',(-0.153648593508749,0.140069200367114,0.978147600733806));
#28691=DIRECTION('ref_axis',(0.722859799300275,-0.658973777457697,0.207911690817759));
#28692=DIRECTION('center_axis',(-0.153648593508749,0.140069200367114,0.978147600733806));
#28693=DIRECTION('ref_axis',(0.722859799300275,-0.658973777457697,0.207911690817759));
#28694=DIRECTION('center_axis',(-0.153648593508749,0.140069200367114,0.978147600733806));
#28695=DIRECTION('ref_axis',(0.722859799300275,-0.658973777457697,0.207911690817759));
#28696=DIRECTION('center_axis',(-0.153648593508749,0.140069200367114,0.978147600733806));
#28697=DIRECTION('ref_axis',(0.722859799300275,-0.658973777457697,0.207911690817759));
#28698=DIRECTION('center_axis',(-0.153648593508749,0.140069200367114,0.978147600733806));
#28699=DIRECTION('ref_axis',(0.722859799300277,-0.658973777457695,0.207911690817759));
#28700=DIRECTION('center_axis',(-0.153648593508749,0.140069200367114,0.978147600733806));
#28701=DIRECTION('ref_axis',(0.722859799300275,-0.658973777457697,0.207911690817759));
#28702=DIRECTION('center_axis',(0.153648593508749,-0.140069200367114,-0.978147600733806));
#28703=DIRECTION('ref_axis',(0.722859799300276,-0.658973777457697,0.207911690817759));
#28704=DIRECTION('center_axis',(-0.153648593508749,0.140069200367114,0.978147600733806));
#28705=DIRECTION('ref_axis',(0.722859799300275,-0.658973777457697,0.207911690817759));
#28706=DIRECTION('center_axis',(0.153648593508749,-0.140069200367114,-0.978147600733806));
#28707=DIRECTION('ref_axis',(0.722859799300276,-0.658973777457697,0.207911690817759));
#28708=DIRECTION('center_axis',(-0.153648593508749,0.140069200367114,0.978147600733806));
#28709=DIRECTION('ref_axis',(0.722859799300275,-0.658973777457697,0.207911690817759));
#28710=DIRECTION('center_axis',(0.,0.,-1.));
#28711=DIRECTION('ref_axis',(-0.739008917220659,0.673695643646558,1.58735880974294E-16));
#28712=DIRECTION('center_axis',(0.153648593508749,-0.140069200367114,-0.978147600733806));
#28713=DIRECTION('ref_axis',(-0.722859799300275,0.658973777457697,-0.207911690817759));
#28714=DIRECTION('center_axis',(-0.0926742152118281,0.186114913463622,0.978147600733806));
#28715=DIRECTION('ref_axis',(0.435997903257853,-0.875601825703931,0.207911690817759));
#28716=DIRECTION('center_axis',(-0.0926742152118281,0.186114913463622,0.978147600733806));
#28717=DIRECTION('ref_axis',(0.435997903257853,-0.875601825703931,0.207911690817759));
#28718=DIRECTION('center_axis',(-0.0926742152118281,0.186114913463622,0.978147600733806));
#28719=DIRECTION('ref_axis',(0.435997903257853,-0.875601825703931,0.207911690817759));
#28720=DIRECTION('center_axis',(-0.0926742152118281,0.186114913463622,0.978147600733806));
#28721=DIRECTION('ref_axis',(0.435997903257853,-0.875601825703931,0.207911690817759));
#28722=DIRECTION('center_axis',(-0.0926742152118281,0.186114913463622,0.978147600733806));
#28723=DIRECTION('ref_axis',(0.435997903257859,-0.875601825703928,0.207911690817759));
#28724=DIRECTION('center_axis',(-0.0926742152118281,0.186114913463622,0.978147600733806));
#28725=DIRECTION('ref_axis',(0.435997903257853,-0.875601825703931,0.207911690817759));
#28726=DIRECTION('center_axis',(0.0926742152118281,-0.186114913463622,-0.978147600733806));
#28727=DIRECTION('ref_axis',(0.435997903257853,-0.875601825703931,0.207911690817759));
#28728=DIRECTION('center_axis',(-0.0926742152118281,0.186114913463622,0.978147600733806));
#28729=DIRECTION('ref_axis',(0.435997903257853,-0.875601825703931,0.207911690817759));
#28730=DIRECTION('center_axis',(0.0926742152118281,-0.186114913463622,-0.978147600733806));
#28731=DIRECTION('ref_axis',(0.435997903257853,-0.875601825703931,0.207911690817759));
#28732=DIRECTION('center_axis',(-0.0926742152118281,0.186114913463622,0.978147600733806));
#28733=DIRECTION('ref_axis',(0.435997903257853,-0.875601825703931,0.207911690817759));
#28734=DIRECTION('center_axis',(0.,0.,-1.));
#28735=DIRECTION('ref_axis',(-0.445738355776558,0.895163291355053,1.58735880974294E-16));
#28736=DIRECTION('center_axis',(0.0926742152118281,-0.186114913463622,-0.978147600733806));
#28737=DIRECTION('ref_axis',(-0.435997903257853,0.875601825703931,-0.207911690817759));
#28738=DIRECTION('center_axis',(-0.0191836706249958,0.207024776198529,0.978147600733806));
#28739=DIRECTION('ref_axis',(0.0902520744326727,-0.97397499551164,0.207911690817759));
#28740=DIRECTION('center_axis',(-0.0191836706249958,0.207024776198529,0.978147600733806));
#28741=DIRECTION('ref_axis',(0.0902520744326727,-0.97397499551164,0.207911690817759));
#28742=DIRECTION('center_axis',(-0.0191836706249958,0.207024776198529,0.978147600733806));
#28743=DIRECTION('ref_axis',(0.0902520744326727,-0.97397499551164,0.207911690817759));
#28744=DIRECTION('center_axis',(-0.0191836706249958,0.207024776198529,0.978147600733806));
#28745=DIRECTION('ref_axis',(0.0902520744326727,-0.97397499551164,0.207911690817759));
#28746=DIRECTION('center_axis',(-0.0191836706249958,0.207024776198529,0.978147600733806));
#28747=DIRECTION('ref_axis',(-0.0902520744326673,0.973974995511641,-0.207911690817759));
#28748=DIRECTION('center_axis',(-0.0191836706249958,0.207024776198529,0.978147600733806));
#28749=DIRECTION('ref_axis',(0.0902520744326727,-0.97397499551164,0.207911690817759));
#28750=DIRECTION('center_axis',(0.0191836706249958,-0.207024776198529,-0.978147600733806));
#28751=DIRECTION('ref_axis',(0.0902520744326727,-0.97397499551164,0.207911690817759));
#28752=DIRECTION('center_axis',(-0.0191836706249958,0.207024776198529,0.978147600733806));
#28753=DIRECTION('ref_axis',(0.0902520744326727,-0.97397499551164,0.207911690817759));
#28754=DIRECTION('center_axis',(0.0191836706249958,-0.207024776198529,-0.978147600733806));
#28755=DIRECTION('ref_axis',(0.0902520744326727,-0.97397499551164,0.207911690817759));
#28756=DIRECTION('center_axis',(-0.0191836706249958,0.207024776198529,0.978147600733806));
#28757=DIRECTION('ref_axis',(0.0902520744326727,-0.97397499551164,0.207911690817759));
#28758=DIRECTION('center_axis',(0.,0.,-1.));
#28759=DIRECTION('ref_axis',(-0.0922683594632729,0.995734176295037,1.58735880974294E-16));
#28760=DIRECTION('center_axis',(0.0191836706249958,-0.207024776198529,-0.978147600733806));
#28761=DIRECTION('ref_axis',(-0.0902520744326727,0.97397499551164,-0.207911690817759));
#28762=DIRECTION('center_axis',(0.0568977349801305,0.19997479574394,0.978147600733806));
#28763=DIRECTION('ref_axis',(-0.267682797148647,-0.940807445193742,0.207911690817759));
#28764=DIRECTION('center_axis',(0.0568977349801305,0.19997479574394,0.978147600733806));
#28765=DIRECTION('ref_axis',(-0.267682797148647,-0.940807445193742,0.207911690817759));
#28766=DIRECTION('center_axis',(0.0568977349801305,0.19997479574394,0.978147600733806));
#28767=DIRECTION('ref_axis',(-0.267682797148647,-0.940807445193742,0.207911690817759));
#28768=DIRECTION('center_axis',(0.0568977349801305,0.19997479574394,0.978147600733806));
#28769=DIRECTION('ref_axis',(-0.267682797148647,-0.940807445193742,0.207911690817759));
#28770=DIRECTION('center_axis',(0.0568977349801305,0.19997479574394,0.978147600733806));
#28771=DIRECTION('ref_axis',(0.267682797148653,0.940807445193741,-0.207911690817759));
#28772=DIRECTION('center_axis',(0.0568977349801305,0.19997479574394,0.978147600733806));
#28773=DIRECTION('ref_axis',(-0.267682797148647,-0.940807445193742,0.207911690817759));
#28774=DIRECTION('center_axis',(-0.0568977349801305,-0.19997479574394,-0.978147600733806));
#28775=DIRECTION('ref_axis',(-0.267682797148647,-0.940807445193742,0.207911690817759));
#28776=DIRECTION('center_axis',(0.0568977349801305,0.19997479574394,0.978147600733806));
#28777=DIRECTION('ref_axis',(-0.267682797148647,-0.940807445193742,0.207911690817759));
#28778=DIRECTION('center_axis',(-0.0568977349801305,-0.19997479574394,-0.978147600733806));
#28779=DIRECTION('ref_axis',(-0.267682797148647,-0.940807445193742,0.207911690817759));
#28780=DIRECTION('center_axis',(0.0568977349801305,0.19997479574394,0.978147600733806));
#28781=DIRECTION('ref_axis',(-0.267682797148647,-0.940807445193742,0.207911690817759));
#28782=DIRECTION('center_axis',(0.,0.,-1.));
#28783=DIRECTION('ref_axis',(0.273662990072067,0.961825643172824,1.58735880974294E-16));
#28784=DIRECTION('center_axis',(-0.0568977349801305,-0.19997479574394,-0.978147600733806));
#28785=DIRECTION('ref_axis',(0.267682797148647,0.940807445193742,-0.207911690817759));
#28786=DIRECTION('center_axis',(0.125294786194957,0.165917111025535,0.978147600733806));
#28787=DIRECTION('ref_axis',(-0.589465623693459,-0.78057863620841,0.207911690817759));
#28788=DIRECTION('center_axis',(0.125294786194957,0.165917111025535,0.978147600733806));
#28789=DIRECTION('ref_axis',(-0.589465623693459,-0.78057863620841,0.207911690817759));
#28790=DIRECTION('center_axis',(0.125294786194957,0.165917111025535,0.978147600733806));
#28791=DIRECTION('ref_axis',(-0.589465623693459,-0.78057863620841,0.207911690817759));
#28792=DIRECTION('center_axis',(0.125294786194957,0.165917111025535,0.978147600733806));
#28793=DIRECTION('ref_axis',(-0.589465623693459,-0.78057863620841,0.207911690817759));
#28794=DIRECTION('center_axis',(0.125294786194957,0.165917111025535,0.978147600733806));
#28795=DIRECTION('ref_axis',(0.589465623693459,0.78057863620841,-0.207911690817759));
#28796=DIRECTION('center_axis',(0.125294786194957,0.165917111025535,0.978147600733806));
#28797=DIRECTION('ref_axis',(-0.589465623693459,-0.78057863620841,0.207911690817759));
#28798=DIRECTION('center_axis',(-0.125294786194957,-0.165917111025535,-0.978147600733806));
#28799=DIRECTION('ref_axis',(-0.589465623693459,-0.78057863620841,0.207911690817759));
#28800=DIRECTION('center_axis',(0.125294786194957,0.165917111025535,0.978147600733806));
#28801=DIRECTION('ref_axis',(-0.589465623693459,-0.78057863620841,0.207911690817759));
#28802=DIRECTION('center_axis',(-0.125294786194957,-0.165917111025535,-0.978147600733806));
#28803=DIRECTION('ref_axis',(-0.589465623693459,-0.78057863620841,0.207911690817759));
#28804=DIRECTION('center_axis',(0.125294786194957,0.165917111025535,0.978147600733806));
#28805=DIRECTION('ref_axis',(-0.589465623693459,-0.78057863620841,0.207911690817759));
#28806=DIRECTION('center_axis',(0.,0.,-1.));
#28807=DIRECTION('ref_axis',(0.602634636379246,0.798017227280247,1.58735880974294E-16));
#28808=DIRECTION('center_axis',(-0.125294786194957,-0.165917111025535,-0.978147600733806));
#28809=DIRECTION('ref_axis',(0.589465623693459,0.78057863620841,-0.207911690817759));
#28810=DIRECTION('center_axis',(0.176770082251776,0.109451401084681,0.978147600733806));
#28811=DIRECTION('ref_axis',(-0.831637851416691,-0.514928357067594,0.207911690817759));
#28812=DIRECTION('center_axis',(0.176770082251776,0.109451401084681,0.978147600733806));
#28813=DIRECTION('ref_axis',(-0.83163785141669,-0.514928357067594,0.207911690817759));
#28814=DIRECTION('center_axis',(0.176770082251776,0.109451401084681,0.978147600733806));
#28815=DIRECTION('ref_axis',(-0.831637851416691,-0.514928357067594,0.207911690817759));
#28816=DIRECTION('center_axis',(0.176770082251776,0.109451401084681,0.978147600733806));
#28817=DIRECTION('ref_axis',(-0.83163785141669,-0.514928357067594,0.207911690817759));
#28818=DIRECTION('center_axis',(0.176770082251776,0.109451401084681,0.978147600733806));
#28819=DIRECTION('ref_axis',(-0.831637851416684,-0.514928357067604,0.207911690817759));
#28820=DIRECTION('center_axis',(0.176770082251776,0.109451401084681,0.978147600733806));
#28821=DIRECTION('ref_axis',(-0.83163785141669,-0.514928357067594,0.207911690817759));
#28822=DIRECTION('center_axis',(-0.176770082251776,-0.109451401084681,-0.978147600733806));
#28823=DIRECTION('ref_axis',(-0.831637851416691,-0.514928357067594,0.207911690817759));
#28824=DIRECTION('center_axis',(0.176770082251776,0.109451401084681,0.978147600733806));
#28825=DIRECTION('ref_axis',(-0.83163785141669,-0.514928357067594,0.207911690817759));
#28826=DIRECTION('center_axis',(-0.176770082251776,-0.109451401084681,-0.978147600733806));
#28827=DIRECTION('ref_axis',(-0.831637851416691,-0.514928357067594,0.207911690817759));
#28828=DIRECTION('center_axis',(0.176770082251776,0.109451401084681,0.978147600733806));
#28829=DIRECTION('ref_axis',(-0.83163785141669,-0.514928357067594,0.207911690817759));
#28830=DIRECTION('center_axis',(0.,0.,-1.));
#28831=DIRECTION('ref_axis',(0.85021713572961,0.526432162877362,1.58735880974294E-16));
#28832=DIRECTION('center_axis',(-0.176770082251776,-0.109451401084681,-0.978147600733806));
#28833=DIRECTION('ref_axis',(0.831637851416691,0.514928357067594,-0.207911690817759));
#28834=DIRECTION('center_axis',(0.204371599183654,0.0382036729361911,0.978147600733806));
#28835=DIRECTION('ref_axis',(-0.961492779041681,-0.179734149988272,0.207911690817759));
#28836=DIRECTION('center_axis',(0.204371599183654,0.0382036729361911,0.978147600733806));
#28837=DIRECTION('ref_axis',(-0.961492779041681,-0.179734149988272,0.207911690817759));
#28838=DIRECTION('center_axis',(0.204371599183654,0.0382036729361911,0.978147600733806));
#28839=DIRECTION('ref_axis',(-0.961492779041681,-0.179734149988272,0.207911690817759));
#28840=DIRECTION('center_axis',(0.204371599183654,0.0382036729361911,0.978147600733806));
#28841=DIRECTION('ref_axis',(-0.961492779041681,-0.179734149988272,0.207911690817759));
#28842=DIRECTION('center_axis',(0.204371599183654,0.0382036729361911,0.978147600733806));
#28843=DIRECTION('ref_axis',(-0.961492779041679,-0.179734149988281,0.207911690817759));
#28844=DIRECTION('center_axis',(0.204371599183654,0.0382036729361911,0.978147600733806));
#28845=DIRECTION('ref_axis',(-0.961492779041681,-0.179734149988272,0.207911690817759));
#28846=DIRECTION('center_axis',(-0.204371599183654,-0.0382036729361911,
-0.978147600733806));
#28847=DIRECTION('ref_axis',(-0.961492779041681,-0.179734149988272,0.207911690817759));
#28848=DIRECTION('center_axis',(0.204371599183654,0.0382036729361911,0.978147600733806));
#28849=DIRECTION('ref_axis',(-0.961492779041681,-0.179734149988272,0.207911690817759));
#28850=DIRECTION('center_axis',(-0.204371599183654,-0.0382036729361911,
-0.978147600733806));
#28851=DIRECTION('ref_axis',(-0.961492779041681,-0.179734149988272,0.207911690817759));
#28852=DIRECTION('center_axis',(0.204371599183654,0.0382036729361911,0.978147600733806));
#28853=DIRECTION('ref_axis',(-0.961492779041681,-0.179734149988272,0.207911690817759));
#28854=DIRECTION('center_axis',(0.,0.,-1.));
#28855=DIRECTION('ref_axis',(0.982973099683894,0.18374951781661,1.58735880974294E-16));
#28856=DIRECTION('center_axis',(-0.204371599183654,-0.0382036729361911,
-0.978147600733806));
#28857=DIRECTION('ref_axis',(0.961492779041681,0.179734149988272,-0.207911690817759));
#28858=DIRECTION('center_axis',(0.204371599183654,-0.0382036729361911,0.978147600733806));
#28859=DIRECTION('ref_axis',(-0.96149277904168,0.179734149988272,0.207911690817759));
#28860=DIRECTION('center_axis',(0.204371599183654,-0.0382036729361911,0.978147600733806));
#28861=DIRECTION('ref_axis',(-0.961492779041681,0.179734149988272,0.207911690817759));
#28862=DIRECTION('center_axis',(0.204371599183654,-0.0382036729361911,0.978147600733806));
#28863=DIRECTION('ref_axis',(-0.96149277904168,0.179734149988272,0.207911690817759));
#28864=DIRECTION('center_axis',(0.204371599183654,-0.0382036729361911,0.978147600733806));
#28865=DIRECTION('ref_axis',(-0.961492779041681,0.179734149988272,0.207911690817759));
#28866=DIRECTION('center_axis',(0.204371599183654,-0.0382036729361911,0.978147600733806));
#28867=DIRECTION('ref_axis',(0.961492779041679,-0.179734149988281,-0.207911690817759));
#28868=DIRECTION('center_axis',(0.204371599183654,-0.0382036729361911,0.978147600733806));
#28869=DIRECTION('ref_axis',(-0.961492779041681,0.179734149988272,0.207911690817759));
#28870=DIRECTION('center_axis',(-0.204371599183654,0.0382036729361911,-0.978147600733806));
#28871=DIRECTION('ref_axis',(-0.961492779041681,0.179734149988272,0.207911690817759));
#28872=DIRECTION('center_axis',(0.204371599183654,-0.0382036729361911,0.978147600733806));
#28873=DIRECTION('ref_axis',(-0.961492779041681,0.179734149988272,0.207911690817759));
#28874=DIRECTION('center_axis',(-0.204371599183654,0.0382036729361911,-0.978147600733806));
#28875=DIRECTION('ref_axis',(-0.961492779041681,0.179734149988272,0.207911690817759));
#28876=DIRECTION('center_axis',(0.204371599183654,-0.0382036729361911,0.978147600733806));
#28877=DIRECTION('ref_axis',(-0.961492779041681,0.179734149988272,0.207911690817759));
#28878=DIRECTION('center_axis',(0.,0.,-1.));
#28879=DIRECTION('ref_axis',(-0.982973099683909,0.183749517816531,1.58735880974294E-16));
#28880=DIRECTION('center_axis',(-0.204371599183654,0.0382036729361911,-0.978147600733806));
#28881=DIRECTION('ref_axis',(0.96149277904168,-0.179734149988272,-0.207911690817759));
#28882=DIRECTION('center_axis',(0.176770082251776,-0.109451401084681,0.978147600733806));
#28883=DIRECTION('ref_axis',(-0.83163785141669,0.514928357067593,0.207911690817759));
#28884=DIRECTION('center_axis',(0.176770082251776,-0.109451401084681,0.978147600733806));
#28885=DIRECTION('ref_axis',(-0.831637851416691,0.514928357067594,0.207911690817759));
#28886=DIRECTION('center_axis',(0.176770082251776,-0.109451401084681,0.978147600733806));
#28887=DIRECTION('ref_axis',(-0.83163785141669,0.514928357067593,0.207911690817759));
#28888=DIRECTION('center_axis',(0.176770082251776,-0.109451401084681,0.978147600733806));
#28889=DIRECTION('ref_axis',(-0.831637851416691,0.514928357067594,0.207911690817759));
#28890=DIRECTION('center_axis',(0.176770082251776,-0.109451401084681,0.978147600733806));
#28891=DIRECTION('ref_axis',(0.831637851416689,-0.514928357067597,-0.207911690817759));
#28892=DIRECTION('center_axis',(0.176770082251776,-0.109451401084681,0.978147600733806));
#28893=DIRECTION('ref_axis',(-0.831637851416691,0.514928357067594,0.207911690817759));
#28894=DIRECTION('center_axis',(-0.176770082251776,0.109451401084681,-0.978147600733806));
#28895=DIRECTION('ref_axis',(-0.831637851416691,0.514928357067593,0.207911690817759));
#28896=DIRECTION('center_axis',(0.176770082251776,-0.109451401084681,0.978147600733806));
#28897=DIRECTION('ref_axis',(-0.831637851416691,0.514928357067594,0.207911690817759));
#28898=DIRECTION('center_axis',(-0.176770082251776,0.109451401084681,-0.978147600733806));
#28899=DIRECTION('ref_axis',(-0.831637851416691,0.514928357067593,0.207911690817759));
#28900=DIRECTION('center_axis',(0.176770082251776,-0.109451401084681,0.978147600733806));
#28901=DIRECTION('ref_axis',(-0.831637851416691,0.514928357067594,0.207911690817759));
#28902=DIRECTION('center_axis',(0.,0.,-1.));
#28903=DIRECTION('ref_axis',(-0.850217135729556,0.52643216287745,1.58735880974294E-16));
#28904=DIRECTION('center_axis',(-0.176770082251776,0.109451401084681,-0.978147600733806));
#28905=DIRECTION('ref_axis',(0.83163785141669,-0.514928357067593,-0.207911690817759));
#28906=DIRECTION('center_axis',(0.125294786194957,-0.165917111025535,0.978147600733806));
#28907=DIRECTION('ref_axis',(-0.589465623693459,0.78057863620841,0.207911690817759));
#28908=DIRECTION('center_axis',(0.125294786194957,-0.165917111025535,0.978147600733806));
#28909=DIRECTION('ref_axis',(-0.589465623693459,0.78057863620841,0.207911690817759));
#28910=DIRECTION('center_axis',(0.125294786194957,-0.165917111025535,0.978147600733806));
#28911=DIRECTION('ref_axis',(-0.589465623693459,0.78057863620841,0.207911690817759));
#28912=DIRECTION('center_axis',(0.125294786194957,-0.165917111025535,0.978147600733806));
#28913=DIRECTION('ref_axis',(-0.589465623693459,0.78057863620841,0.207911690817759));
#28914=DIRECTION('center_axis',(0.125294786194957,-0.165917111025535,0.978147600733806));
#28915=DIRECTION('ref_axis',(0.589465623693453,-0.780578636208415,-0.207911690817759));
#28916=DIRECTION('center_axis',(0.125294786194957,-0.165917111025535,0.978147600733806));
#28917=DIRECTION('ref_axis',(-0.589465623693459,0.78057863620841,0.207911690817759));
#28918=DIRECTION('center_axis',(-0.125294786194957,0.165917111025535,-0.978147600733806));
#28919=DIRECTION('ref_axis',(-0.589465623693459,0.78057863620841,0.207911690817759));
#28920=DIRECTION('center_axis',(0.125294786194957,-0.165917111025535,0.978147600733806));
#28921=DIRECTION('ref_axis',(-0.589465623693459,0.78057863620841,0.207911690817759));
#28922=DIRECTION('center_axis',(-0.125294786194957,0.165917111025535,-0.978147600733806));
#28923=DIRECTION('ref_axis',(-0.589465623693459,0.78057863620841,0.207911690817759));
#28924=DIRECTION('center_axis',(0.125294786194957,-0.165917111025535,0.978147600733806));
#28925=DIRECTION('ref_axis',(-0.589465623693459,0.78057863620841,0.207911690817759));
#28926=DIRECTION('center_axis',(0.,0.,-1.));
#28927=DIRECTION('ref_axis',(-0.602634636379309,0.7980172272802,1.58735880974294E-16));
#28928=DIRECTION('center_axis',(-0.125294786194957,0.165917111025535,-0.978147600733806));
#28929=DIRECTION('ref_axis',(0.589465623693459,-0.78057863620841,-0.207911690817759));
#28930=DIRECTION('center_axis',(0.0568977349801304,-0.19997479574394,0.978147600733806));
#28931=DIRECTION('ref_axis',(-0.267682797148647,0.940807445193742,0.207911690817759));
#28932=DIRECTION('center_axis',(0.0568977349801304,-0.19997479574394,0.978147600733806));
#28933=DIRECTION('ref_axis',(-0.267682797148647,0.940807445193742,0.207911690817759));
#28934=DIRECTION('center_axis',(0.0568977349801304,-0.19997479574394,0.978147600733806));
#28935=DIRECTION('ref_axis',(-0.267682797148647,0.940807445193742,0.207911690817759));
#28936=DIRECTION('center_axis',(0.0568977349801304,-0.19997479574394,0.978147600733806));
#28937=DIRECTION('ref_axis',(-0.267682797148647,0.940807445193742,0.207911690817759));
#28938=DIRECTION('center_axis',(0.0568977349801304,-0.19997479574394,0.978147600733806));
#28939=DIRECTION('ref_axis',(0.267682797148644,-0.940807445193743,-0.207911690817759));
#28940=DIRECTION('center_axis',(0.0568977349801304,-0.19997479574394,0.978147600733806));
#28941=DIRECTION('ref_axis',(-0.267682797148647,0.940807445193742,0.207911690817759));
#28942=DIRECTION('center_axis',(-0.0568977349801304,0.19997479574394,-0.978147600733806));
#28943=DIRECTION('ref_axis',(-0.267682797148647,0.940807445193742,0.207911690817759));
#28944=DIRECTION('center_axis',(0.0568977349801304,-0.19997479574394,0.978147600733806));
#28945=DIRECTION('ref_axis',(-0.267682797148647,0.940807445193742,0.207911690817759));
#28946=DIRECTION('center_axis',(-0.0568977349801304,0.19997479574394,-0.978147600733806));
#28947=DIRECTION('ref_axis',(-0.267682797148647,0.940807445193742,0.207911690817759));
#28948=DIRECTION('center_axis',(0.0568977349801304,-0.19997479574394,0.978147600733806));
#28949=DIRECTION('ref_axis',(-0.267682797148647,0.940807445193742,0.207911690817759));
#28950=DIRECTION('center_axis',(0.,0.,-1.));
#28951=DIRECTION('ref_axis',(-0.273662990072115,0.96182564317281,1.58735880974294E-16));
#28952=DIRECTION('center_axis',(-0.0568977349801304,0.19997479574394,-0.978147600733806));
#28953=DIRECTION('ref_axis',(0.267682797148647,-0.940807445193742,-0.207911690817759));
#28954=DIRECTION('center_axis',(-0.0191836706249959,-0.207024776198529,
0.978147600733806));
#28955=DIRECTION('ref_axis',(0.0902520744326732,0.97397499551164,0.207911690817759));
#28956=DIRECTION('center_axis',(-0.0191836706249959,-0.207024776198529,
0.978147600733806));
#28957=DIRECTION('ref_axis',(0.0902520744326732,0.97397499551164,0.207911690817759));
#28958=DIRECTION('center_axis',(-0.0191836706249959,-0.207024776198529,
0.978147600733806));
#28959=DIRECTION('ref_axis',(0.0902520744326732,0.97397499551164,0.207911690817759));
#28960=DIRECTION('center_axis',(-0.0191836706249959,-0.207024776198529,
0.978147600733806));
#28961=DIRECTION('ref_axis',(0.0902520744326732,0.97397499551164,0.207911690817759));
#28962=DIRECTION('center_axis',(-0.0191836706249959,-0.207024776198529,
0.978147600733806));
#28963=DIRECTION('ref_axis',(-0.0902520744326954,-0.973974995511638,-0.207911690817759));
#28964=DIRECTION('center_axis',(-0.0191836706249959,-0.207024776198529,
0.978147600733806));
#28965=DIRECTION('ref_axis',(0.0902520744326732,0.97397499551164,0.207911690817759));
#28966=DIRECTION('center_axis',(0.0191836706249959,0.207024776198529,-0.978147600733806));
#28967=DIRECTION('ref_axis',(0.0902520744326732,0.97397499551164,0.207911690817759));
#28968=DIRECTION('center_axis',(-0.0191836706249959,-0.207024776198529,
0.978147600733806));
#28969=DIRECTION('ref_axis',(0.0902520744326732,0.97397499551164,0.207911690817759));
#28970=DIRECTION('center_axis',(0.0191836706249959,0.207024776198529,-0.978147600733806));
#28971=DIRECTION('ref_axis',(0.0902520744326732,0.97397499551164,0.207911690817759));
#28972=DIRECTION('center_axis',(-0.0191836706249959,-0.207024776198529,
0.978147600733806));
#28973=DIRECTION('ref_axis',(0.0902520744326732,0.97397499551164,0.207911690817759));
#28974=DIRECTION('center_axis',(0.,0.,-1.));
#28975=DIRECTION('ref_axis',(0.0922683594632895,0.995734176295036,1.58735880974294E-16));
#28976=DIRECTION('center_axis',(0.0191836706249959,0.207024776198529,-0.978147600733806));
#28977=DIRECTION('ref_axis',(-0.0902520744326732,-0.97397499551164,-0.207911690817759));
#28978=DIRECTION('center_axis',(-0.092674215211828,-0.186114913463622,0.978147600733806));
#28979=DIRECTION('ref_axis',(0.435997903257852,0.875601825703931,0.207911690817759));
#28980=DIRECTION('center_axis',(-0.092674215211828,-0.186114913463622,0.978147600733806));
#28981=DIRECTION('ref_axis',(0.435997903257852,0.875601825703931,0.207911690817759));
#28982=DIRECTION('center_axis',(-0.092674215211828,-0.186114913463622,0.978147600733806));
#28983=DIRECTION('ref_axis',(0.435997903257852,0.875601825703931,0.207911690817759));
#28984=DIRECTION('center_axis',(-0.092674215211828,-0.186114913463622,0.978147600733806));
#28985=DIRECTION('ref_axis',(0.435997903257852,0.875601825703931,0.207911690817759));
#28986=DIRECTION('center_axis',(-0.092674215211828,-0.186114913463622,0.978147600733806));
#28987=DIRECTION('ref_axis',(-0.435997903257876,-0.875601825703919,-0.207911690817759));
#28988=DIRECTION('center_axis',(-0.092674215211828,-0.186114913463622,0.978147600733806));
#28989=DIRECTION('ref_axis',(0.435997903257852,0.875601825703931,0.207911690817759));
#28990=DIRECTION('center_axis',(0.092674215211828,0.186114913463622,-0.978147600733806));
#28991=DIRECTION('ref_axis',(0.435997903257852,0.875601825703931,0.207911690817759));
#28992=DIRECTION('center_axis',(-0.092674215211828,-0.186114913463622,0.978147600733806));
#28993=DIRECTION('ref_axis',(0.435997903257852,0.875601825703931,0.207911690817759));
#28994=DIRECTION('center_axis',(0.092674215211828,0.186114913463622,-0.978147600733806));
#28995=DIRECTION('ref_axis',(0.435997903257852,0.875601825703931,0.207911690817759));
#28996=DIRECTION('center_axis',(-0.092674215211828,-0.186114913463622,0.978147600733806));
#28997=DIRECTION('ref_axis',(0.435997903257852,0.875601825703931,0.207911690817759));
#28998=DIRECTION('center_axis',(0.,0.,-1.));
#28999=DIRECTION('ref_axis',(0.445738355776574,0.895163291355045,1.58735880974294E-16));
#29000=DIRECTION('center_axis',(0.092674215211828,0.186114913463622,-0.978147600733806));
#29001=DIRECTION('ref_axis',(-0.435997903257852,-0.875601825703931,-0.207911690817759));
#29002=DIRECTION('center_axis',(-0.153648593508749,-0.140069200367114,0.978147600733806));
#29003=DIRECTION('ref_axis',(0.722859799300275,0.658973777457697,0.207911690817759));
#29004=DIRECTION('center_axis',(-0.153648593508749,-0.140069200367114,0.978147600733806));
#29005=DIRECTION('ref_axis',(0.722859799300275,0.658973777457697,0.207911690817759));
#29006=DIRECTION('center_axis',(-0.153648593508749,-0.140069200367114,0.978147600733806));
#29007=DIRECTION('ref_axis',(0.722859799300275,0.658973777457697,0.207911690817759));
#29008=DIRECTION('center_axis',(-0.153648593508749,-0.140069200367114,0.978147600733806));
#29009=DIRECTION('ref_axis',(0.722859799300275,0.658973777457697,0.207911690817759));
#29010=DIRECTION('center_axis',(-0.153648593508749,-0.140069200367114,0.978147600733806));
#29011=DIRECTION('ref_axis',(0.722859799300273,0.658973777457699,0.207911690817759));
#29012=DIRECTION('center_axis',(-0.153648593508749,-0.140069200367114,0.978147600733806));
#29013=DIRECTION('ref_axis',(0.722859799300275,0.658973777457697,0.207911690817759));
#29014=DIRECTION('center_axis',(0.153648593508749,0.140069200367114,-0.978147600733806));
#29015=DIRECTION('ref_axis',(0.722859799300275,0.658973777457697,0.207911690817759));
#29016=DIRECTION('center_axis',(-0.153648593508749,-0.140069200367114,0.978147600733806));
#29017=DIRECTION('ref_axis',(0.722859799300275,0.658973777457697,0.207911690817759));
#29018=DIRECTION('center_axis',(0.153648593508749,0.140069200367114,-0.978147600733806));
#29019=DIRECTION('ref_axis',(0.722859799300275,0.658973777457697,0.207911690817759));
#29020=DIRECTION('center_axis',(-0.153648593508749,-0.140069200367114,0.978147600733806));
#29021=DIRECTION('ref_axis',(0.722859799300275,0.658973777457697,0.207911690817759));
#29022=DIRECTION('center_axis',(0.,0.,-1.));
#29023=DIRECTION('ref_axis',(0.739008917220659,0.673695643646557,1.58735880974294E-16));
#29024=DIRECTION('center_axis',(0.153648593508749,0.140069200367114,-0.978147600733806));
#29025=DIRECTION('ref_axis',(-0.722859799300275,-0.658973777457697,-0.207911690817759));
#29026=DIRECTION('center_axis',(-0.193871877856065,-0.0751063656107956,
0.978147600733806));
#29027=DIRECTION('ref_axis',(0.912095473942774,0.353347669066046,0.207911690817759));
#29028=DIRECTION('center_axis',(-0.193871877856065,-0.0751063656107956,
0.978147600733806));
#29029=DIRECTION('ref_axis',(0.912095473942774,0.353347669066046,0.207911690817759));
#29030=DIRECTION('center_axis',(-0.193871877856065,-0.0751063656107956,
0.978147600733806));
#29031=DIRECTION('ref_axis',(0.912095473942774,0.353347669066046,0.207911690817759));
#29032=DIRECTION('center_axis',(-0.193871877856065,-0.0751063656107956,
0.978147600733806));
#29033=DIRECTION('ref_axis',(0.912095473942774,0.353347669066046,0.207911690817759));
#29034=DIRECTION('center_axis',(-0.193871877856065,-0.0751063656107956,
0.978147600733806));
#29035=DIRECTION('ref_axis',(-0.912095473942778,-0.353347669066033,-0.207911690817759));
#29036=DIRECTION('center_axis',(-0.193871877856065,-0.0751063656107956,
0.978147600733806));
#29037=DIRECTION('ref_axis',(0.912095473942774,0.353347669066046,0.207911690817759));
#29038=DIRECTION('center_axis',(0.193871877856065,0.0751063656107956,-0.978147600733806));
#29039=DIRECTION('ref_axis',(0.912095473942773,0.353347669066046,0.207911690817759));
#29040=DIRECTION('center_axis',(-0.193871877856065,-0.0751063656107956,
0.978147600733806));
#29041=DIRECTION('ref_axis',(0.912095473942773,0.353347669066046,0.207911690817759));
#29042=DIRECTION('center_axis',(0.193871877856065,0.0751063656107956,-0.978147600733806));
#29043=DIRECTION('ref_axis',(0.912095473942773,0.353347669066046,0.207911690817759));
#29044=DIRECTION('center_axis',(-0.193871877856065,-0.0751063656107956,
0.978147600733806));
#29045=DIRECTION('ref_axis',(0.912095473942773,0.353347669066046,0.207911690817759));
#29046=DIRECTION('center_axis',(0.,0.,-1.));
#29047=DIRECTION('ref_axis',(0.932472229404352,0.361241666187163,1.58735880974294E-16));
#29048=DIRECTION('center_axis',(0.193871877856065,0.0751063656107956,-0.978147600733806));
#29049=DIRECTION('ref_axis',(-0.912095473942774,-0.353347669066046,-0.207911690817759));
#29050=DIRECTION('center_axis',(0.207911690817759,0.,-0.978147600733806));
#29051=DIRECTION('ref_axis',(-0.978147600733806,0.,-0.207911690817759));
#29052=DIRECTION('center_axis',(-0.207911690817759,0.,0.978147600733806));
#29053=DIRECTION('ref_axis',(0.978147600733806,0.,0.207911690817759));
#29054=DIRECTION('center_axis',(-0.207911690817759,0.,0.978147600733806));
#29055=DIRECTION('ref_axis',(0.978147600733806,0.,0.207911690817759));
#29056=DIRECTION('center_axis',(-0.207911690817759,0.,0.978147600733806));
#29057=DIRECTION('ref_axis',(0.978147600733806,0.,0.207911690817759));
#29058=DIRECTION('center_axis',(-0.207911690817759,0.,0.978147600733806));
#29059=DIRECTION('ref_axis',(0.978147600733806,0.,0.207911690817759));
#29060=DIRECTION('center_axis',(-0.207911690817759,0.,0.978147600733806));
#29061=DIRECTION('ref_axis',(0.978147600733806,0.,0.207911690817759));
#29062=DIRECTION('center_axis',(-0.207911690817759,0.,0.978147600733806));
#29063=DIRECTION('ref_axis',(0.978147600733806,1.96011575733601E-14,0.207911690817759));
#29064=DIRECTION('center_axis',(-0.207911690817759,0.,0.978147600733806));
#29065=DIRECTION('ref_axis',(0.978147600733806,0.,0.207911690817759));
#29066=DIRECTION('center_axis',(0.207911690817759,0.,-0.978147600733806));
#29067=DIRECTION('ref_axis',(0.978147600733806,0.,0.207911690817759));
#29068=DIRECTION('center_axis',(0.207911690817759,0.,-0.978147600733806));
#29069=DIRECTION('ref_axis',(0.978147600733806,0.,0.207911690817759));
#29070=DIRECTION('center_axis',(-0.207911690817759,0.,0.978147600733806));
#29071=DIRECTION('ref_axis',(0.978147600733806,0.,0.207911690817759));
#29072=DIRECTION('center_axis',(0.,0.,-1.));
#29073=DIRECTION('ref_axis',(1.,8.77688512853447E-14,1.58735880974294E-16));
#29074=DIRECTION('center_axis',(0.193871877856065,-0.0751063656107956,-0.978147600733806));
#29075=DIRECTION('ref_axis',(-0.912095473942774,0.353347669066046,-0.207911690817759));
#29076=DIRECTION('center_axis',(-0.193871877856065,0.0751063656107956,0.978147600733806));
#29077=DIRECTION('ref_axis',(0.912095473942773,-0.353347669066046,0.207911690817759));
#29078=DIRECTION('',(-0.361241666187153,-0.932472229404356,0.));
#29079=DIRECTION('center_axis',(0.193871877856065,-0.0751063656107956,-0.978147600733806));
#29080=DIRECTION('ref_axis',(0.912095473942773,-0.353347669066046,0.207911690817759));
#29081=DIRECTION('center_axis',(0.,0.,-1.));
#29082=DIRECTION('ref_axis',(-0.932472229404348,0.361241666187173,1.58735880974294E-16));
#29083=DIRECTION('center_axis',(0.,0.,-1.));
#29084=DIRECTION('ref_axis',(1.,0.,0.));
#29085=DIRECTION('center_axis',(0.,0.,1.));
#29086=DIRECTION('ref_axis',(1.,0.,0.));
#29087=DIRECTION('',(-0.173648177666931,-2.12657684957577E-17,-0.984807753012208));
#29088=DIRECTION('center_axis',(0.,0.,1.));
#29089=DIRECTION('ref_axis',(1.,0.,0.));
#29090=DIRECTION('center_axis',(0.,0.,1.));
#29091=DIRECTION('ref_axis',(1.,0.,0.));
#29092=DIRECTION('center_axis',(0.,0.,1.));
#29093=DIRECTION('ref_axis',(1.,0.,0.));
#29094=DIRECTION('center_axis',(0.,0.,1.));
#29095=DIRECTION('ref_axis',(1.,0.,0.));
#29096=DIRECTION('center_axis',(0.,0.,1.));
#29097=DIRECTION('ref_axis',(1.,0.,0.));
#29098=DIRECTION('center_axis',(0.,0.,1.));
#29099=DIRECTION('ref_axis',(1.,0.,0.));
#29100=DIRECTION('center_axis',(0.,0.,1.));
#29101=DIRECTION('ref_axis',(1.,0.,0.));
#29102=DIRECTION('center_axis',(0.,0.,1.));
#29103=DIRECTION('ref_axis',(1.,0.,0.));
#29104=DIRECTION('center_axis',(0.,0.,1.));
#29105=DIRECTION('ref_axis',(1.,0.,0.));
#29106=DIRECTION('center_axis',(0.,0.,1.));
#29107=DIRECTION('ref_axis',(1.,0.,0.));
#29108=DIRECTION('center_axis',(0.,0.,1.));
#29109=DIRECTION('ref_axis',(1.,0.,0.));
#29110=DIRECTION('center_axis',(0.,0.,1.));
#29111=DIRECTION('ref_axis',(1.,0.,0.));
#29112=DIRECTION('center_axis',(0.,0.,1.));
#29113=DIRECTION('ref_axis',(1.,0.,0.));
#29114=DIRECTION('center_axis',(0.,0.,1.));
#29115=DIRECTION('ref_axis',(1.,0.,0.));
#29116=DIRECTION('center_axis',(0.,0.,1.));
#29117=DIRECTION('ref_axis',(1.,0.,0.));
#29118=DIRECTION('center_axis',(0.,0.,1.));
#29119=DIRECTION('ref_axis',(1.,0.,0.));
#29120=DIRECTION('center_axis',(0.,0.,1.));
#29121=DIRECTION('ref_axis',(1.,0.,0.));
#29122=DIRECTION('center_axis',(0.,0.,1.));
#29123=DIRECTION('ref_axis',(1.,0.,0.));
#29124=DIRECTION('center_axis',(0.153648593508749,-0.140069200367114,-0.978147600733806));
#29125=DIRECTION('ref_axis',(-0.722859799300275,0.658973777457697,-0.207911690817759));
#29126=DIRECTION('center_axis',(-0.153648593508749,0.140069200367114,0.978147600733806));
#29127=DIRECTION('ref_axis',(0.722859799300275,-0.658973777457697,0.207911690817759));
#29128=DIRECTION('',(-0.673695643646557,-0.739008917220659,0.));
#29129=DIRECTION('center_axis',(0.153648593508749,-0.140069200367114,-0.978147600733806));
#29130=DIRECTION('ref_axis',(0.722859799300276,-0.658973777457697,0.207911690817759));
#29131=DIRECTION('center_axis',(0.,0.,-1.));
#29132=DIRECTION('ref_axis',(-0.739008917220659,0.673695643646558,1.58735880974294E-16));
#29133=DIRECTION('center_axis',(0.0926742152118281,-0.186114913463622,-0.978147600733806));
#29134=DIRECTION('ref_axis',(-0.435997903257853,0.875601825703931,-0.207911690817759));
#29135=DIRECTION('center_axis',(-0.0926742152118281,0.186114913463622,0.978147600733806));
#29136=DIRECTION('ref_axis',(0.435997903257853,-0.875601825703931,0.207911690817759));
#29137=DIRECTION('',(-0.895163291355062,-0.445738355776538,0.));
#29138=DIRECTION('center_axis',(0.0926742152118281,-0.186114913463622,-0.978147600733806));
#29139=DIRECTION('ref_axis',(0.435997903257853,-0.875601825703931,0.207911690817759));
#29140=DIRECTION('center_axis',(0.,0.,-1.));
#29141=DIRECTION('ref_axis',(-0.445738355776558,0.895163291355053,1.58735880974294E-16));
#29142=DIRECTION('center_axis',(0.0191836706249958,-0.207024776198529,-0.978147600733806));
#29143=DIRECTION('ref_axis',(-0.0902520744326727,0.97397499551164,-0.207911690817759));
#29144=DIRECTION('center_axis',(-0.0191836706249958,0.207024776198529,0.978147600733806));
#29145=DIRECTION('ref_axis',(0.0902520744326727,-0.97397499551164,0.207911690817759));
#29146=DIRECTION('',(-0.995734176295035,-0.0922683594633015,0.));
#29147=DIRECTION('center_axis',(0.0191836706249958,-0.207024776198529,-0.978147600733806));
#29148=DIRECTION('ref_axis',(0.0902520744326727,-0.97397499551164,0.207911690817759));
#29149=DIRECTION('center_axis',(0.,0.,-1.));
#29150=DIRECTION('ref_axis',(-0.0922683594632729,0.995734176295037,1.58735880974294E-16));
#29151=DIRECTION('center_axis',(-0.0568977349801305,-0.19997479574394,-0.978147600733806));
#29152=DIRECTION('ref_axis',(0.267682797148647,0.940807445193742,-0.207911690817759));
#29153=DIRECTION('center_axis',(0.0568977349801305,0.19997479574394,0.978147600733806));
#29154=DIRECTION('ref_axis',(-0.267682797148647,-0.940807445193742,0.207911690817759));
#29155=DIRECTION('',(-0.961825643172819,0.273662990072083,0.));
#29156=DIRECTION('center_axis',(-0.0568977349801305,-0.19997479574394,-0.978147600733806));
#29157=DIRECTION('ref_axis',(-0.267682797148647,-0.940807445193742,0.207911690817759));
#29158=DIRECTION('center_axis',(0.,0.,-1.));
#29159=DIRECTION('ref_axis',(0.273662990072067,0.961825643172824,1.58735880974294E-16));
#29160=DIRECTION('center_axis',(-0.125294786194957,-0.165917111025535,-0.978147600733806));
#29161=DIRECTION('ref_axis',(0.589465623693459,0.78057863620841,-0.207911690817759));
#29162=DIRECTION('center_axis',(0.125294786194957,0.165917111025535,0.978147600733806));
#29163=DIRECTION('ref_axis',(-0.589465623693459,-0.78057863620841,0.207911690817759));
#29164=DIRECTION('',(-0.798017227280239,0.602634636379257,0.));
#29165=DIRECTION('center_axis',(-0.125294786194957,-0.165917111025535,-0.978147600733806));
#29166=DIRECTION('ref_axis',(-0.589465623693459,-0.78057863620841,0.207911690817759));
#29167=DIRECTION('center_axis',(0.,0.,-1.));
#29168=DIRECTION('ref_axis',(0.602634636379246,0.798017227280247,1.58735880974294E-16));
#29169=DIRECTION('center_axis',(-0.176770082251776,-0.109451401084681,-0.978147600733806));
#29170=DIRECTION('ref_axis',(0.831637851416691,0.514928357067594,-0.207911690817759));
#29171=DIRECTION('center_axis',(0.176770082251776,0.109451401084681,0.978147600733806));
#29172=DIRECTION('ref_axis',(-0.83163785141669,-0.514928357067594,0.207911690817759));
#29173=DIRECTION('',(-0.526432162877356,0.850217135729614,0.));
#29174=DIRECTION('center_axis',(-0.176770082251776,-0.109451401084681,-0.978147600733806));
#29175=DIRECTION('ref_axis',(-0.831637851416691,-0.514928357067594,0.207911690817759));
#29176=DIRECTION('center_axis',(0.,0.,-1.));
#29177=DIRECTION('ref_axis',(0.85021713572961,0.526432162877362,1.58735880974294E-16));
#29178=DIRECTION('center_axis',(-0.204371599183654,-0.0382036729361911,
-0.978147600733806));
#29179=DIRECTION('ref_axis',(0.961492779041681,0.179734149988272,-0.207911690817759));
#29180=DIRECTION('center_axis',(0.204371599183654,0.0382036729361911,0.978147600733806));
#29181=DIRECTION('ref_axis',(-0.961492779041681,-0.179734149988272,0.207911690817759));
#29182=DIRECTION('',(-0.18374951781657,0.982973099683902,0.));
#29183=DIRECTION('center_axis',(-0.204371599183654,-0.0382036729361911,
-0.978147600733806));
#29184=DIRECTION('ref_axis',(-0.961492779041681,-0.179734149988272,0.207911690817759));
#29185=DIRECTION('center_axis',(0.,0.,-1.));
#29186=DIRECTION('ref_axis',(0.982973099683894,0.18374951781661,1.58735880974294E-16));
#29187=DIRECTION('center_axis',(-0.204371599183654,0.0382036729361911,-0.978147600733806));
#29188=DIRECTION('ref_axis',(0.96149277904168,-0.179734149988272,-0.207911690817759));
#29189=DIRECTION('center_axis',(0.204371599183654,-0.0382036729361911,0.978147600733806));
#29190=DIRECTION('ref_axis',(-0.961492779041681,0.179734149988272,0.207911690817759));
#29191=DIRECTION('',(0.18374951781657,0.982973099683902,0.));
#29192=DIRECTION('center_axis',(-0.204371599183654,0.0382036729361911,-0.978147600733806));
#29193=DIRECTION('ref_axis',(-0.961492779041681,0.179734149988272,0.207911690817759));
#29194=DIRECTION('center_axis',(0.,0.,-1.));
#29195=DIRECTION('ref_axis',(-0.982973099683909,0.183749517816531,1.58735880974294E-16));
#29196=DIRECTION('center_axis',(-0.176770082251776,0.109451401084681,-0.978147600733806));
#29197=DIRECTION('ref_axis',(0.83163785141669,-0.514928357067593,-0.207911690817759));
#29198=DIRECTION('center_axis',(0.176770082251776,-0.109451401084681,0.978147600733806));
#29199=DIRECTION('ref_axis',(-0.831637851416691,0.514928357067594,0.207911690817759));
#29200=DIRECTION('',(0.526432162877356,0.850217135729614,0.));
#29201=DIRECTION('center_axis',(-0.176770082251776,0.109451401084681,-0.978147600733806));
#29202=DIRECTION('ref_axis',(-0.831637851416691,0.514928357067593,0.207911690817759));
#29203=DIRECTION('center_axis',(0.,0.,-1.));
#29204=DIRECTION('ref_axis',(-0.850217135729556,0.52643216287745,1.58735880974294E-16));
#29205=DIRECTION('center_axis',(-0.125294786194957,0.165917111025535,-0.978147600733806));
#29206=DIRECTION('ref_axis',(0.589465623693459,-0.78057863620841,-0.207911690817759));
#29207=DIRECTION('center_axis',(0.125294786194957,-0.165917111025535,0.978147600733806));
#29208=DIRECTION('ref_axis',(-0.589465623693459,0.78057863620841,0.207911690817759));
#29209=DIRECTION('',(0.79801722728024,0.602634636379256,0.));
#29210=DIRECTION('center_axis',(-0.125294786194957,0.165917111025535,-0.978147600733806));
#29211=DIRECTION('ref_axis',(-0.589465623693459,0.78057863620841,0.207911690817759));
#29212=DIRECTION('center_axis',(0.,0.,-1.));
#29213=DIRECTION('ref_axis',(-0.602634636379309,0.7980172272802,1.58735880974294E-16));
#29214=DIRECTION('center_axis',(-0.0568977349801304,0.19997479574394,-0.978147600733806));
#29215=DIRECTION('ref_axis',(0.267682797148647,-0.940807445193742,-0.207911690817759));
#29216=DIRECTION('center_axis',(0.0568977349801304,-0.19997479574394,0.978147600733806));
#29217=DIRECTION('ref_axis',(-0.267682797148647,0.940807445193742,0.207911690817759));
#29218=DIRECTION('',(0.961825643172819,0.273662990072083,0.));
#29219=DIRECTION('center_axis',(-0.0568977349801304,0.19997479574394,-0.978147600733806));
#29220=DIRECTION('ref_axis',(-0.267682797148647,0.940807445193742,0.207911690817759));
#29221=DIRECTION('center_axis',(0.,0.,-1.));
#29222=DIRECTION('ref_axis',(-0.273662990072115,0.96182564317281,1.58735880974294E-16));
#29223=DIRECTION('center_axis',(0.0191836706249959,0.207024776198529,-0.978147600733806));
#29224=DIRECTION('ref_axis',(-0.0902520744326732,-0.97397499551164,-0.207911690817759));
#29225=DIRECTION('center_axis',(-0.0191836706249959,-0.207024776198529,
0.978147600733806));
#29226=DIRECTION('ref_axis',(0.0902520744326732,0.97397499551164,0.207911690817759));
#29227=DIRECTION('',(0.995734176295035,-0.092268359463302,0.));
#29228=DIRECTION('center_axis',(0.0191836706249959,0.207024776198529,-0.978147600733806));
#29229=DIRECTION('ref_axis',(0.0902520744326732,0.97397499551164,0.207911690817759));
#29230=DIRECTION('center_axis',(0.,0.,-1.));
#29231=DIRECTION('ref_axis',(0.0922683594632895,0.995734176295036,1.58735880974294E-16));
#29232=DIRECTION('center_axis',(0.092674215211828,0.186114913463622,-0.978147600733806));
#29233=DIRECTION('ref_axis',(-0.435997903257852,-0.875601825703931,-0.207911690817759));
#29234=DIRECTION('center_axis',(-0.092674215211828,-0.186114913463622,0.978147600733806));
#29235=DIRECTION('ref_axis',(0.435997903257852,0.875601825703931,0.207911690817759));
#29236=DIRECTION('',(0.895163291355062,-0.445738355776538,0.));
#29237=DIRECTION('center_axis',(0.092674215211828,0.186114913463622,-0.978147600733806));
#29238=DIRECTION('ref_axis',(0.435997903257852,0.875601825703931,0.207911690817759));
#29239=DIRECTION('center_axis',(0.,0.,-1.));
#29240=DIRECTION('ref_axis',(0.445738355776574,0.895163291355045,1.58735880974294E-16));
#29241=DIRECTION('center_axis',(0.153648593508749,0.140069200367114,-0.978147600733806));
#29242=DIRECTION('ref_axis',(-0.722859799300275,-0.658973777457697,-0.207911690817759));
#29243=DIRECTION('center_axis',(-0.153648593508749,-0.140069200367114,0.978147600733806));
#29244=DIRECTION('ref_axis',(0.722859799300275,0.658973777457697,0.207911690817759));
#29245=DIRECTION('',(0.673695643646557,-0.739008917220659,0.));
#29246=DIRECTION('center_axis',(0.153648593508749,0.140069200367114,-0.978147600733806));
#29247=DIRECTION('ref_axis',(0.722859799300275,0.658973777457697,0.207911690817759));
#29248=DIRECTION('center_axis',(0.,0.,-1.));
#29249=DIRECTION('ref_axis',(0.739008917220659,0.673695643646557,1.58735880974294E-16));
#29250=DIRECTION('center_axis',(0.193871877856065,0.0751063656107956,-0.978147600733806));
#29251=DIRECTION('ref_axis',(-0.912095473942774,-0.353347669066046,-0.207911690817759));
#29252=DIRECTION('center_axis',(-0.193871877856065,-0.0751063656107956,
0.978147600733806));
#29253=DIRECTION('ref_axis',(0.912095473942773,0.353347669066046,0.207911690817759));
#29254=DIRECTION('',(0.361241666187153,-0.932472229404356,0.));
#29255=DIRECTION('center_axis',(0.193871877856065,0.0751063656107956,-0.978147600733806));
#29256=DIRECTION('ref_axis',(0.912095473942773,0.353347669066046,0.207911690817759));
#29257=DIRECTION('center_axis',(0.,0.,-1.));
#29258=DIRECTION('ref_axis',(0.932472229404352,0.361241666187163,1.58735880974294E-16));
#29259=DIRECTION('center_axis',(0.207911690817759,0.,-0.978147600733806));
#29260=DIRECTION('ref_axis',(0.978147600733806,0.,0.207911690817759));
#29261=DIRECTION('center_axis',(0.,0.,-1.));
#29262=DIRECTION('ref_axis',(1.,8.77688512853447E-14,1.58735880974294E-16));
#29263=DIRECTION('center_axis',(-0.207911690817759,0.,0.978147600733806));
#29264=DIRECTION('ref_axis',(0.978147600733806,0.,0.207911690817759));
#29265=DIRECTION('center_axis',(0.207911690817759,0.,-0.978147600733806));
#29266=DIRECTION('ref_axis',(-0.978147600733806,0.,-0.207911690817759));
#29267=DIRECTION('',(0.,-1.,0.));
#29268=DIRECTION('center_axis',(0.,0.,-1.));
#29269=DIRECTION('ref_axis',(1.,0.,0.));
#29270=DIRECTION('center_axis',(0.,0.,1.));
#29271=DIRECTION('ref_axis',(1.,0.,0.));
#29272=DIRECTION('',(-0.707106781186548,-8.65956056235494E-17,-0.707106781186547));
#29273=DIRECTION('center_axis',(0.,0.,1.));
#29274=DIRECTION('ref_axis',(1.,0.,0.));
#29275=DIRECTION('center_axis',(0.,0.,-1.));
#29276=DIRECTION('ref_axis',(-1.,0.,0.));
#29277=DIRECTION('center_axis',(0.,0.,1.));
#29278=DIRECTION('ref_axis',(1.,0.,0.));
#29279=DIRECTION('center_axis',(0.,0.,1.));
#29280=DIRECTION('ref_axis',(1.,0.,0.));
#29281=DIRECTION('center_axis',(0.,0.,1.));
#29282=DIRECTION('ref_axis',(1.,0.,0.));
#29283=DIRECTION('',(0.707106781186548,8.65956056235494E-17,-0.707106781186547));
#29284=DIRECTION('center_axis',(0.,0.,1.));
#29285=DIRECTION('ref_axis',(1.,0.,0.));
#29286=DIRECTION('center_axis',(0.,0.,1.));
#29287=DIRECTION('ref_axis',(1.,0.,0.));
#29288=DIRECTION('',(0.,0.,-1.));
#29289=DIRECTION('center_axis',(0.,0.,1.));
#29290=DIRECTION('ref_axis',(1.,0.,0.));
#29291=DIRECTION('center_axis',(0.,0.,-1.));
#29292=DIRECTION('ref_axis',(-1.,0.,0.));
#29293=DIRECTION('center_axis',(0.,0.,1.));
#29294=DIRECTION('ref_axis',(1.,0.,0.));
#29295=DIRECTION('center_axis',(0.,0.,1.));
#29296=DIRECTION('ref_axis',(1.,0.,0.));
#29297=DIRECTION('center_axis',(0.,0.,1.));
#29298=DIRECTION('ref_axis',(1.,0.,0.));
#29299=DIRECTION('',(0.,0.,-1.));
#29300=DIRECTION('center_axis',(0.,0.,1.));
#29301=DIRECTION('ref_axis',(1.,0.,0.));
#29302=DIRECTION('center_axis',(0.,0.,1.));
#29303=DIRECTION('ref_axis',(1.,0.,0.));
#29304=DIRECTION('center_axis',(0.,0.,1.));
#29305=DIRECTION('ref_axis',(1.,0.,0.));
#29306=DIRECTION('',(0.707106781186547,8.65956056235493E-17,-0.707106781186547));
#29307=DIRECTION('center_axis',(0.,0.,1.));
#29308=DIRECTION('ref_axis',(1.,0.,0.));
#29309=DIRECTION('center_axis',(0.,0.,1.));
#29310=DIRECTION('ref_axis',(1.,0.,0.));
#29311=DIRECTION('',(0.,0.,-1.));
#47402=CARTESIAN_POINT('',(0.,0.,0.));
#47403=CARTESIAN_POINT('Origin',(0.,0.,0.817011318356283));
#47404=CARTESIAN_POINT('',(-1.75488973075546,-2.14912009162623E-16,1.44791652082959));
#47405=CARTESIAN_POINT('Origin',(0.,0.,1.44791652082959));
#47406=CARTESIAN_POINT('',(-2.02309581191037,-2.47757781042445E-16,0.186106115882978));
#47407=CARTESIAN_POINT('',(-1.88899277133291,-2.31334895102534E-16,0.817011318356283));
#47408=CARTESIAN_POINT('Origin',(0.,0.,0.186106115882978));
#47409=CARTESIAN_POINT('',(1.96553101732603,-0.404034822633264,0.263580625276104));
#47410=CARTESIAN_POINT('',(1.72474144876727,-1.02558434703109,0.263580625276103));
#47411=CARTESIAN_POINT('Origin',(-0.0884849938604435,0.0342792692444314,
-0.177187331777248));
#47412=CARTESIAN_POINT('',(1.73109633135173,-0.356297004039415,1.38914111564877));
#47413=CARTESIAN_POINT('Ctrl Pts',(1.96553101732603,-0.404034822633264,
0.263580625276103));
#47414=CARTESIAN_POINT('Ctrl Pts',(1.88793646815053,-0.388221893764485,
0.636136973435854));
#47415=CARTESIAN_POINT('Ctrl Pts',(1.80874957916707,-0.37209543523409,1.0163282025572));
#47416=CARTESIAN_POINT('Ctrl Pts',(1.73109633135173,-0.356297004039416,
1.38914111564877));
#47417=CARTESIAN_POINT('',(1.51933136490257,-0.902925394000066,1.38914111564877));
#47418=CARTESIAN_POINT('Origin',(-0.0779352888697595,0.0301922917576571,
1.00090915210539));
#47419=CARTESIAN_POINT('Ctrl Pts',(1.51933136490257,-0.902925394000065,
1.38914111564877));
#47420=CARTESIAN_POINT('Ctrl Pts',(1.58736114175433,-0.94356486723299,1.01632820259676));
#47421=CARTESIAN_POINT('Ctrl Pts',(1.65674528369834,-0.984995132717264,
0.636136973481484));
#47422=CARTESIAN_POINT('Ctrl Pts',(1.72474144876727,-1.02558434703109,0.263580625276103));
#47423=CARTESIAN_POINT('',(1.68684887716375,-1.08678295145922,0.263580625276104));
#47424=CARTESIAN_POINT('',(1.23778970554114,-1.57937739721302,0.263580625276103));
#47425=CARTESIAN_POINT('Origin',(-0.0701266991563423,0.063928933229414,
-0.177187331777248));
#47426=CARTESIAN_POINT('',(1.48548993201256,-0.957581184754694,1.38914111564877));
#47427=CARTESIAN_POINT('Ctrl Pts',(1.68684887716375,-1.08678295145922,0.263580625276104));
#47428=CARTESIAN_POINT('Ctrl Pts',(1.62014150671713,-1.04396579507641,0.636499771706221));
#47429=CARTESIAN_POINT('Ctrl Pts',(1.55215789194248,-1.00034225256772,1.0165209491176));
#47430=CARTESIAN_POINT('Ctrl Pts',(1.48548993201256,-0.957581184754693,
1.38914111564877));
#47431=CARTESIAN_POINT('',(1.09056003126339,-1.39079864887685,1.38914111564877));
#47432=CARTESIAN_POINT('Origin',(-0.0617657787811128,0.0563069472121782,
1.00090915210539));
#47433=CARTESIAN_POINT('Ctrl Pts',(1.09056003126339,-1.39079864887685,1.38914111564877));
#47434=CARTESIAN_POINT('Ctrl Pts',(1.13929003118602,-1.45323672146031,1.01652094915712));
#47435=CARTESIAN_POINT('Ctrl Pts',(1.18900021995803,-1.51690525741751,0.636499771750218));
#47436=CARTESIAN_POINT('Ctrl Pts',(1.23778970554114,-1.57937739721302,0.263580625276103));
#47437=CARTESIAN_POINT('',(1.18034844898819,-1.62275502061838,0.263580625276103));
#47438=CARTESIAN_POINT('',(0.583667603752152,-1.91986677826906,0.263580625276103));
#47439=CARTESIAN_POINT('Origin',(-0.0422974051457228,0.0849446405393159,
-0.177187331777248));
#47440=CARTESIAN_POINT('',(1.03925988597122,-1.42953872032833,1.38914111564877));
#47441=CARTESIAN_POINT('Ctrl Pts',(1.18034844898819,-1.62275502061838,0.263580625276103));
#47442=CARTESIAN_POINT('Ctrl Pts',(1.1336409924622,-1.55877005016848,0.636276564880181));
#47443=CARTESIAN_POINT('Ctrl Pts',(1.08599375050078,-1.49351590217855,1.01640192898384));
#47444=CARTESIAN_POINT('Ctrl Pts',(1.03925988597122,-1.42953872032833,1.38914111564877));
#47445=CARTESIAN_POINT('',(0.514502522400341,-1.69083683954147,1.38914111564877));
#47446=CARTESIAN_POINT('Origin',(-0.0372544580120808,0.0748170374381298,
1.00090915210539));
#47447=CARTESIAN_POINT('Ctrl Pts',(0.514502522400341,-1.69083683954147,
1.38914111564877));
#47448=CARTESIAN_POINT('Ctrl Pts',(0.537393970209863,-1.76668613424626,
1.0164019290234));
#47449=CARTESIAN_POINT('Ctrl Pts',(0.560754026123086,-1.8440338639089,0.636276564925202));
#47450=CARTESIAN_POINT('Ctrl Pts',(0.583667603752152,-1.91986677826906,
0.263580625276104));
#47451=CARTESIAN_POINT('',(0.514435422240241,-1.93956503224705,0.263580625276104));
#47452=CARTESIAN_POINT('',(-0.149282042137411,-2.0010675125708,0.263580625276104));
#47453=CARTESIAN_POINT('Origin',(-0.00875561219215992,0.0944881034498817,
-0.177187331777248));
#47454=CARTESIAN_POINT('',(0.452672033591646,-1.70842913037413,1.38914111564877));
#47455=CARTESIAN_POINT('Ctrl Pts',(0.514435422240241,-1.93956503224705,
0.263580625276104));
#47456=CARTESIAN_POINT('Ctrl Pts',(0.4940205153564,-1.86311974435583,0.6358305212866));
#47457=CARTESIAN_POINT('Ctrl Pts',(0.473150118322512,-1.78501046959186,
1.01619654162157));
#47458=CARTESIAN_POINT('Ctrl Pts',(0.452672033591646,-1.70842913037413,
1.38914111564877));
#47459=CARTESIAN_POINT('',(-0.131041403069769,-1.76251814577564,1.38914111564877));
#47460=CARTESIAN_POINT('Origin',(-0.00771171625443978,0.0832226721825453,
1.00090915210539));
#47461=CARTESIAN_POINT('Ctrl Pts',(-0.131041403069769,-1.76251814577564,
1.38914111564877));
#47462=CARTESIAN_POINT('Ctrl Pts',(-0.137099025337607,-1.84155838035113,
1.01619654166127));
#47463=CARTESIAN_POINT('Ctrl Pts',(-0.143261522626645,-1.92217262167001,
0.63583052133358));
#47464=CARTESIAN_POINT('Ctrl Pts',(-0.149282042137411,-2.0010675125708,
0.263580625276104));
#47465=CARTESIAN_POINT('',(-0.220954958866336,-1.9944260387699,0.263580625276103));
#47466=CARTESIAN_POINT('',(-0.862070321035964,-1.81201299100198,0.263580625276103));
#47467=CARTESIAN_POINT('Origin',(0.0259686747044756,0.0912704244128846,
-0.177187331777247));
#47468=CARTESIAN_POINT('',(-0.195051685266811,-1.75658671963028,1.38914111564877));
#47469=CARTESIAN_POINT('Ctrl Pts',(-0.220954958866336,-1.9944260387699,
0.263580625276103));
#47470=CARTESIAN_POINT('Ctrl Pts',(-0.212371888991068,-1.91572988628875,
0.636011916383804));
#47471=CARTESIAN_POINT('Ctrl Pts',(-0.203619189092551,-1.83537931742317,
1.0162671092937));
#47472=CARTESIAN_POINT('Ctrl Pts',(-0.195051685266812,-1.75658671963028,
1.38914111564877));
#47473=CARTESIAN_POINT('',(-0.758887460929825,-1.59616160997261,1.38914111564877));
#47474=CARTESIAN_POINT('Origin',(0.0228725355154589,0.0803886238959624,
1.00090915210539));
#47475=CARTESIAN_POINT('Ctrl Pts',(-0.758887460929825,-1.59616160997261,
1.38914111564877));
#47476=CARTESIAN_POINT('Ctrl Pts',(-0.79308218003796,-1.66766263634664,
1.01626710933327));
#47477=CARTESIAN_POINT('Ctrl Pts',(-0.827939608356074,-1.7405857695991,
0.636011916429978));
#47478=CARTESIAN_POINT('Ctrl Pts',(-0.862070321035964,-1.81201299100198,
0.263580625276103));
#47479=CARTESIAN_POINT('',(-0.92650414842432,-1.77992875726067,0.263580625276104));
#47480=CARTESIAN_POINT('',(-1.45843122618206,-1.37823607428775,0.263580625276103));
#47481=CARTESIAN_POINT('Origin',(0.0571857481848785,0.0757261688120474,
-0.177187331777248));
#47482=CARTESIAN_POINT('',(-0.816432593211287,-1.56750753881733,1.38914111564877));
#47483=CARTESIAN_POINT('Ctrl Pts',(-0.926504148424321,-1.77992875726068,
0.263580625276104));
#47484=CARTESIAN_POINT('Ctrl Pts',(-0.890024902524132,-1.70955582085882,
0.636496905193193));
#47485=CARTESIAN_POINT('Ctrl Pts',(-0.852859726540045,-1.63783625100815,
1.01652279052734));
#47486=CARTESIAN_POINT('Ctrl Pts',(-0.816432593211287,-1.56750753881733,
1.38914111564877));
#47487=CARTESIAN_POINT('',(-1.28424156205072,-1.21423460410598,1.38914111564877));
#47488=CARTESIAN_POINT('Origin',(0.0503677246228997,0.0666976465034872,
1.00090915210539));
#47489=CARTESIAN_POINT('Ctrl Pts',(-1.28424156205072,-1.21423460410598,
1.38914111564877));
#47490=CARTESIAN_POINT('Ctrl Pts',(-1.34191676265454,-1.26851752070915,
1.01652279056689));
#47491=CARTESIAN_POINT('Ctrl Pts',(-1.4007277508672,-1.32389093193504,0.63649690523722));
#47492=CARTESIAN_POINT('Ctrl Pts',(-1.45843122618206,-1.37823607428775,
0.263580625276104));
#47493=CARTESIAN_POINT('',(-1.50692381880089,-1.32504223415768,0.263580625276104));
#47494=CARTESIAN_POINT('',(-1.85782291278586,-0.758320738671227,0.263580625276103));
#47495=CARTESIAN_POINT('Origin',(0.080679569495743,0.0499546744999564,-0.177187331777248));
#47496=CARTESIAN_POINT('',(-1.32754975543341,-1.16672777902799,1.38914111564877));
#47497=CARTESIAN_POINT('Ctrl Pts',(-1.50692381880088,-1.32504223415768,
0.263580625276104));
#47498=CARTESIAN_POINT('Ctrl Pts',(-1.44749808261794,-1.27260964643021,
0.636422969016795));
#47499=CARTESIAN_POINT('Ctrl Pts',(-1.38692897637993,-1.21915388714204,
1.01648344351096));
#47500=CARTESIAN_POINT('Ctrl Pts',(-1.32754975543341,-1.16672777902799,
1.38914111564877));
#47501=CARTESIAN_POINT('',(-1.63615172398851,-0.668318486648626,1.38914111564877));
#47502=CARTESIAN_POINT('Origin',(0.0710604734228215,0.0439987823662984,
1.00090915210539));
#47503=CARTESIAN_POINT('Ctrl Pts',(-1.63615172398851,-0.668318486648626,
1.38914111564877));
#47504=CARTESIAN_POINT('Ctrl Pts',(-1.70954924778502,-0.698104258275537,
1.01648344355053));
#47505=CARTESIAN_POINT('Ctrl Pts',(-1.78439885503574,-0.728496216517704,
0.636422969061169));
#47506=CARTESIAN_POINT('Ctrl Pts',(-1.85782291278586,-0.758320738671227,
0.263580625276103));
#47507=CARTESIAN_POINT('',(-1.88382507729525,-0.691201415019197,0.263580625276104));
#47508=CARTESIAN_POINT('',(-2.00630532046579,-0.0359899852968828,0.263580625276104));
#47509=CARTESIAN_POINT('Origin',(0.0932771678852804,0.0174365245882386,
-0.177187331777248));
#47510=CARTESIAN_POINT('',(-1.6593739669771,-0.608374967619113,1.38914111564877));
#47511=CARTESIAN_POINT('Ctrl Pts',(-1.88382507729525,-0.691201415019197,
0.263580625276104));
#47512=CARTESIAN_POINT('Ctrl Pts',(-1.80957400607897,-0.663814383089077,
0.635908422736754));
#47513=CARTESIAN_POINT('Ctrl Pts',(-1.73373386455056,-0.635829781577252,
1.01622302039257));
#47514=CARTESIAN_POINT('Ctrl Pts',(-1.6593739669771,-0.608374967619113,
1.38914111564877));
#47515=CARTESIAN_POINT('',(-1.76709052937197,-0.0321422542887969,1.38914111564877));
#47516=CARTESIAN_POINT('Origin',(0.0821561115273148,0.0153576388648713,
1.00090915210539));
#47517=CARTESIAN_POINT('Ctrl Pts',(-1.76709052937197,-0.032142254288797,
1.38914111564877));
#47518=CARTESIAN_POINT('Ctrl Pts',(-1.84634689157125,-0.0334032960061751,
1.01622302043219));
#47519=CARTESIAN_POINT('Ctrl Pts',(-1.92717492149681,-0.0347050513350173,
0.635908422783382));
#47520=CARTESIAN_POINT('Ctrl Pts',(-2.00630532046579,-0.0359899852968828,
0.263580625276103));
#47521=CARTESIAN_POINT('',(-2.00630532046579,0.0359899852968833,0.263580625276103));
#47522=CARTESIAN_POINT('',(-1.88382507729525,0.691201415019197,0.263580625276103));
#47523=CARTESIAN_POINT('Origin',(0.0932771678852804,-0.0174365245882386,
-0.177187331777248));
#47524=CARTESIAN_POINT('',(-1.76709052937197,0.0321422542887974,1.38914111564877));
#47525=CARTESIAN_POINT('Ctrl Pts',(-2.00630532046579,0.0359899852968834,
0.263580625276103));
#47526=CARTESIAN_POINT('Ctrl Pts',(-1.92717492150672,0.0347050513351788,
0.635908422736753));
#47527=CARTESIAN_POINT('Ctrl Pts',(-1.84634689157967,0.0334032960063096,
1.01622302039257));
#47528=CARTESIAN_POINT('Ctrl Pts',(-1.76709052937197,0.0321422542887974,
1.38914111564877));
#47529=CARTESIAN_POINT('',(-1.6593739669771,0.608374967619113,1.38914111564877));
#47530=CARTESIAN_POINT('Origin',(0.0821561115273148,-0.0153576388648713,
1.00090915210539));
#47531=CARTESIAN_POINT('Ctrl Pts',(-1.6593739669771,0.608374967619113,1.38914111564877));
#47532=CARTESIAN_POINT('Ctrl Pts',(-1.73373386454266,0.635829781574335,
1.01622302043219));
#47533=CARTESIAN_POINT('Ctrl Pts',(-1.80957400606967,0.663814383085648,
0.635908422783382));
#47534=CARTESIAN_POINT('Ctrl Pts',(-1.88382507729525,0.691201415019197,
0.263580625276103));
#47535=CARTESIAN_POINT('',(-1.85782291278586,0.758320738671226,0.263580625276104));
#47536=CARTESIAN_POINT('',(-1.50692381880089,1.32504223415768,0.263580625276103));
#47537=CARTESIAN_POINT('Origin',(0.0806795694957425,-0.0499546744999564,
-0.177187331777248));
#47538=CARTESIAN_POINT('',(-1.63615172398851,0.668318486648626,1.38914111564877));
#47539=CARTESIAN_POINT('Ctrl Pts',(-1.85782291278586,0.758320738671226,
0.263580625276104));
#47540=CARTESIAN_POINT('Ctrl Pts',(-1.78439885504448,0.728496216521253,
0.636422969016796));
#47541=CARTESIAN_POINT('Ctrl Pts',(-1.70954924779282,0.698104258278699,
1.01648344351096));
#47542=CARTESIAN_POINT('Ctrl Pts',(-1.63615172398851,0.668318486648626,
1.38914111564877));
#47543=CARTESIAN_POINT('',(-1.32754975543341,1.16672777902799,1.38914111564877));
#47544=CARTESIAN_POINT('Origin',(0.0710604734228211,-0.0439987823662986,
1.00090915210539));
#47545=CARTESIAN_POINT('Ctrl Pts',(-1.32754975543341,1.16672777902799,1.38914111564877));
#47546=CARTESIAN_POINT('Ctrl Pts',(-1.38692897637363,1.21915388713648,1.01648344355052));
#47547=CARTESIAN_POINT('Ctrl Pts',(-1.44749808261087,1.27260964642397,0.636422969061169));
#47548=CARTESIAN_POINT('Ctrl Pts',(-1.50692381880089,1.32504223415768,0.263580625276103));
#47549=CARTESIAN_POINT('',(-1.45843122618206,1.37823607428775,0.263580625276103));
#47550=CARTESIAN_POINT('',(-0.92650414842432,1.77992875726068,0.263580625276103));
#47551=CARTESIAN_POINT('Origin',(0.0571857481848781,-0.0757261688120474,
-0.177187331777248));
#47552=CARTESIAN_POINT('',(-1.28424156205072,1.21423460410598,1.38914111564877));
#47553=CARTESIAN_POINT('Ctrl Pts',(-1.45843122618206,1.37823607428775,0.263580625276103));
#47554=CARTESIAN_POINT('Ctrl Pts',(-1.40072775087401,1.32389093194146,0.636496905193193));
#47555=CARTESIAN_POINT('Ctrl Pts',(-1.34191676266067,1.26851752071491,1.01652279052734));
#47556=CARTESIAN_POINT('Ctrl Pts',(-1.28424156205072,1.21423460410598,1.38914111564877));
#47557=CARTESIAN_POINT('',(-0.816432593211287,1.56750753881733,1.38914111564877));
#47558=CARTESIAN_POINT('Origin',(0.0503677246229,-0.066697646503487,1.00090915210539));
#47559=CARTESIAN_POINT('Ctrl Pts',(-0.816432593211287,1.56750753881734,
1.38914111564877));
#47560=CARTESIAN_POINT('Ctrl Pts',(-0.852859726536179,1.63783625100069,
1.01652279056688));
#47561=CARTESIAN_POINT('Ctrl Pts',(-0.890024902519824,1.70955582085052,
0.63649690523722));
#47562=CARTESIAN_POINT('Ctrl Pts',(-0.92650414842432,1.77992875726068,0.263580625276103));
#47563=CARTESIAN_POINT('',(-0.862070321035964,1.81201299100198,0.263580625276104));
#47564=CARTESIAN_POINT('',(-0.220954958866335,1.9944260387699,0.263580625276103));
#47565=CARTESIAN_POINT('Origin',(0.0259686747044761,-0.091270424412885,
-0.177187331777248));
#47566=CARTESIAN_POINT('',(-0.758887460929825,1.59616160997261,1.38914111564877));
#47567=CARTESIAN_POINT('Ctrl Pts',(-0.862070321035964,1.81201299100198,
0.263580625276104));
#47568=CARTESIAN_POINT('Ctrl Pts',(-0.827939608360305,1.74058576960796,
0.636011916383804));
#47569=CARTESIAN_POINT('Ctrl Pts',(-0.793082180041589,1.66766263635423,
1.0162671092937));
#47570=CARTESIAN_POINT('Ctrl Pts',(-0.758887460929825,1.59616160997261,
1.38914111564877));
#47571=CARTESIAN_POINT('',(-0.195051685266811,1.75658671963028,1.38914111564877));
#47572=CARTESIAN_POINT('Origin',(0.0228725355154586,-0.0803886238959621,
1.00090915210539));
#47573=CARTESIAN_POINT('Ctrl Pts',(-0.195051685266811,1.75658671963028,
1.38914111564877));
#47574=CARTESIAN_POINT('Ctrl Pts',(-0.203619189091641,1.83537931741481,
1.01626710933327));
#47575=CARTESIAN_POINT('Ctrl Pts',(-0.212371888990004,1.91572988627899,
0.636011916429979));
#47576=CARTESIAN_POINT('Ctrl Pts',(-0.220954958866335,1.9944260387699,0.263580625276103));
#47577=CARTESIAN_POINT('',(-0.14928204213741,2.0010675125708,0.263580625276104));
#47578=CARTESIAN_POINT('',(0.514435422240242,1.93956503224705,0.263580625276103));
#47579=CARTESIAN_POINT('Origin',(-0.00875561219215948,-0.0944881034498812,
-0.177187331777248));
#47580=CARTESIAN_POINT('',(-0.131041403069769,1.76251814577564,1.38914111564877));
#47581=CARTESIAN_POINT('Ctrl Pts',(-0.14928204213741,2.0010675125708,0.263580625276104));
#47582=CARTESIAN_POINT('Ctrl Pts',(-0.143261522627404,1.92217262167996,
0.635830521286599));
#47583=CARTESIAN_POINT('Ctrl Pts',(-0.137099025338251,1.84155838035954,
1.01619654162157));
#47584=CARTESIAN_POINT('Ctrl Pts',(-0.131041403069769,1.76251814577564,
1.38914111564877));
#47585=CARTESIAN_POINT('',(0.452672033591647,1.70842913037412,1.38914111564877));
#47586=CARTESIAN_POINT('Origin',(-0.00771171625443956,-0.0832226721825451,
1.00090915210539));
#47587=CARTESIAN_POINT('Ctrl Pts',(0.452672033591647,1.70842913037413,1.38914111564877));
#47588=CARTESIAN_POINT('Ctrl Pts',(0.473150118320333,1.78501046958371,1.01619654166127));
#47589=CARTESIAN_POINT('Ctrl Pts',(0.494020515353825,1.86311974434618,0.63583052133358));
#47590=CARTESIAN_POINT('Ctrl Pts',(0.514435422240242,1.93956503224705,0.263580625276104));
#47591=CARTESIAN_POINT('',(0.583667603752152,1.91986677826906,0.263580625276103));
#47592=CARTESIAN_POINT('',(1.18034844898819,1.62275502061838,0.263580625276103));
#47593=CARTESIAN_POINT('Origin',(-0.0422974051457223,-0.0849446405393151,
-0.177187331777248));
#47594=CARTESIAN_POINT('',(0.514502522400341,1.69083683954147,1.38914111564877));
#47595=CARTESIAN_POINT('Ctrl Pts',(0.583667603752152,1.91986677826906,0.263580625276104));
#47596=CARTESIAN_POINT('Ctrl Pts',(0.560754026125854,1.84403386391806,0.636276564880181));
#47597=CARTESIAN_POINT('Ctrl Pts',(0.537393970212291,1.76668613425431,1.01640192898384));
#47598=CARTESIAN_POINT('Ctrl Pts',(0.514502522400341,1.69083683954147,1.38914111564877));
#47599=CARTESIAN_POINT('',(1.03925988597122,1.42953872032833,1.38914111564877));
#47600=CARTESIAN_POINT('Origin',(-0.0372544580120806,-0.074817037438129,
1.00090915210539));
#47601=CARTESIAN_POINT('Ctrl Pts',(1.03925988597122,1.42953872032833,1.38914111564877));
#47602=CARTESIAN_POINT('Ctrl Pts',(1.08599375049582,1.49351590217177,1.0164019290234));
#47603=CARTESIAN_POINT('Ctrl Pts',(1.13364099245656,1.55877005016075,0.636276564925202));
#47604=CARTESIAN_POINT('Ctrl Pts',(1.18034844898819,1.62275502061838,0.263580625276103));
#47605=CARTESIAN_POINT('',(1.23778970554114,1.57937739721302,0.263580625276104));
#47606=CARTESIAN_POINT('',(1.68684887716375,1.08678295145922,0.263580625276104));
#47607=CARTESIAN_POINT('Origin',(-0.0701266991563427,-0.0639289332294135,
-0.177187331777248));
#47608=CARTESIAN_POINT('',(1.09056003126339,1.39079864887685,1.38914111564877));
#47609=CARTESIAN_POINT('Ctrl Pts',(1.23778970554114,1.57937739721302,0.263580625276103));
#47610=CARTESIAN_POINT('Ctrl Pts',(1.1890002199638,1.51690525742489,0.636499771706133));
#47611=CARTESIAN_POINT('Ctrl Pts',(1.1392900311912,1.45323672146694,1.01652094911755));
#47612=CARTESIAN_POINT('Ctrl Pts',(1.09056003126339,1.39079864887685,1.38914111564877));
#47613=CARTESIAN_POINT('',(1.48548993201256,0.957581184754693,1.38914111564877));
#47614=CARTESIAN_POINT('Origin',(-0.061765778781113,-0.0563069472121784,
1.00090915210539));
#47615=CARTESIAN_POINT('Ctrl Pts',(1.48548993201256,0.957581184754694,1.38914111564877));
#47616=CARTESIAN_POINT('Ctrl Pts',(1.55215789193542,1.00034225256319,1.01652094915707));
#47617=CARTESIAN_POINT('Ctrl Pts',(1.62014150670928,1.04396579507136,0.636499771750131));
#47618=CARTESIAN_POINT('Ctrl Pts',(1.68684887716375,1.08678295145922,0.263580625276104));
#47619=CARTESIAN_POINT('',(1.72474144876727,1.02558434703109,0.263580625276104));
#47620=CARTESIAN_POINT('',(1.96553101732603,0.404034822633264,0.263580625276104));
#47621=CARTESIAN_POINT('Origin',(-0.0884849938604444,-0.0342792692444314,
-0.177187331777248));
#47622=CARTESIAN_POINT('',(1.51933136490257,0.902925394000065,1.38914111564877));
#47623=CARTESIAN_POINT('Ctrl Pts',(1.72474144876727,1.02558434703109,0.263580625276104));
#47624=CARTESIAN_POINT('Ctrl Pts',(1.6567452837067,0.984995132722253,0.636136973435691));
#47625=CARTESIAN_POINT('Ctrl Pts',(1.58736114176157,0.943564867237314,1.0163282025571));
#47626=CARTESIAN_POINT('Ctrl Pts',(1.51933136490257,0.902925394000065,1.38914111564877));
#47627=CARTESIAN_POINT('',(1.73109633135173,0.356297004039415,1.38914111564877));
#47628=CARTESIAN_POINT('Origin',(-0.07793528886976,-0.0301922917576571,
1.00090915210539));
#47629=CARTESIAN_POINT('Ctrl Pts',(1.73109633135173,0.356297004039415,1.38914111564877));
#47630=CARTESIAN_POINT('Ctrl Pts',(1.80874957915885,0.372095435232418,1.01632820259666));
#47631=CARTESIAN_POINT('Ctrl Pts',(1.88793646814106,0.388221893762555,0.636136973481322));
#47632=CARTESIAN_POINT('Ctrl Pts',(1.96553101732603,0.404034822633264,0.263580625276104));
#47633=CARTESIAN_POINT('',(1.97875730221509,0.333280447823553,0.263580625276104));
#47634=CARTESIAN_POINT('',(1.74290857880594,0.293107061381241,1.38914111564877));
#47635=CARTESIAN_POINT('Ctrl Pts',(1.97875730221509,0.333280447823553,0.263580625276103));
#47636=CARTESIAN_POINT('Ctrl Pts',(1.90076305042376,0.320007569431509,0.635789556457961));
#47637=CARTESIAN_POINT('Ctrl Pts',(1.82105162804574,0.306431570368061,1.01620172824913));
#47638=CARTESIAN_POINT('Ctrl Pts',(1.74290857880594,0.293107061381241,1.38914111564877));
#47639=CARTESIAN_POINT('',(1.74290857880594,-0.293107061381241,1.38914111564877));
#47640=CARTESIAN_POINT('Origin',(-0.0835792063422023,-4.44089209850063E-16,
1.00090915210539));
#47641=CARTESIAN_POINT('',(1.97875730221509,-0.333280447823553,0.263580625276104));
#47642=CARTESIAN_POINT('Ctrl Pts',(1.74290857880594,-0.293107061381241,
1.38914111564877));
#47643=CARTESIAN_POINT('Ctrl Pts',(1.82105162803739,-0.306431570366637,
1.01620172828898));
#47644=CARTESIAN_POINT('Ctrl Pts',(1.90076305041387,-0.320007569429825,
0.635789556505179));
#47645=CARTESIAN_POINT('Ctrl Pts',(1.97875730221509,-0.333280447823553,
0.263580625276104));
#47646=CARTESIAN_POINT('Origin',(-0.0948928998314158,-4.44089209850063E-16,
-0.177187331777248));
#47647=CARTESIAN_POINT('Origin',(0.,0.,0.833644253621703));
#47648=CARTESIAN_POINT('',(-1.83314153881416,-2.24495091789282E-16,1.46454945609501));
#47649=CARTESIAN_POINT('Origin',(0.,0.,1.46454945609501));
#47650=CARTESIAN_POINT('',(-2.10134761996907,-2.57340863669103E-16,0.202739051148399));
#47651=CARTESIAN_POINT('',(-1.96724457939162,-2.40917977729193E-16,0.833644253621703));
#47652=CARTESIAN_POINT('Origin',(0.,0.,0.202739051148399));
#47653=CARTESIAN_POINT('',(1.79536793495708,-1.0598953697797,0.280213560541524));
#47654=CARTESIAN_POINT('',(2.04083980696707,-0.426259426935219,0.280213560541524));
#47655=CARTESIAN_POINT('Origin',(-0.0919376867122903,0.0356168495811988,
-0.177974371324324));
#47656=CARTESIAN_POINT('',(1.58996439658141,-0.937219520893876,1.4057740509142));
#47657=CARTESIAN_POINT('Ctrl Pts',(1.79536793495708,-1.0598953697797,0.280213560541524));
#47658=CARTESIAN_POINT('Ctrl Pts',(1.72736598254189,-1.01929689490354,0.652811627092658));
#47659=CARTESIAN_POINT('Ctrl Pts',(1.65800091965806,-0.977871183631695,
1.03291010040004));
#47660=CARTESIAN_POINT('Ctrl Pts',(1.58996439658141,-0.937219520893876,
1.4057740509142));
#47661=CARTESIAN_POINT('',(1.80639857550374,-0.378538504196173,1.4057740509142));
#47662=CARTESIAN_POINT('Origin',(-0.0813879817216061,0.0315298720944248,
1.00012211255832));
#47663=CARTESIAN_POINT('Ctrl Pts',(1.80639857550374,-0.378538504196173,
1.4057740509142));
#47664=CARTESIAN_POINT('Ctrl Pts',(1.88406502083852,-0.394332472136845,
1.03291010044331));
#47665=CARTESIAN_POINT('Ctrl Pts',(1.96323474207058,-0.410449442790543,
0.652811627142982));
#47666=CARTESIAN_POINT('Ctrl Pts',(2.04083980696707,-0.426259426935219,
0.280213560541524));
#47667=CARTESIAN_POINT('',(1.29125237154726,-1.63688470263671,0.280213560541524));
#47668=CARTESIAN_POINT('',(1.74904377904568,-1.13471145042876,0.280213560541524));
#47669=CARTESIAN_POINT('Origin',(-0.0728630496078391,0.0664234462666804,
-0.177974371324323));
#47670=CARTESIAN_POINT('',(1.14403490424299,-1.44829256388851,1.4057740509142));
#47671=CARTESIAN_POINT('Ctrl Pts',(1.29125237154726,-1.63688470263671,0.280213560541524));
#47672=CARTESIAN_POINT('Ctrl Pts',(1.24247685283117,-1.57442234203435,0.653052008848893));
#47673=CARTESIAN_POINT('Ctrl Pts',(1.19277667894508,-1.51075710516702,1.03302725266647));
#47674=CARTESIAN_POINT('Ctrl Pts',(1.14403490424299,-1.44829256388851,1.4057740509142));
#47675=CARTESIAN_POINT('',(1.54767262692101,-1.00552307413627,1.4057740509142));
#47676=CARTESIAN_POINT('Origin',(-0.0645021292326089,0.0588014602494451,
1.00012211255832));
#47677=CARTESIAN_POINT('Ctrl Pts',(1.54767262692101,-1.00552307413627,1.4057740509142));
#47678=CARTESIAN_POINT('Ctrl Pts',(1.61436802906001,-1.04829342426708,1.03302725270948));
#47679=CARTESIAN_POINT('Ctrl Pts',(1.68234743475918,-1.09190729901199,0.653052008897806));
#47680=CARTESIAN_POINT('Ctrl Pts',(1.74904377904568,-1.13471145042876,0.280213560541524));
#47681=CARTESIAN_POINT('',(0.612746020283587,-1.99280368611139,0.280213560541524));
#47682=CARTESIAN_POINT('',(1.22102969697802,-1.68991440488869,0.280213560541524));
#47683=CARTESIAN_POINT('Origin',(-0.043947853905753,0.0882591884688249,
-0.177974371324323));
#47684=CARTESIAN_POINT('',(0.543597158770307,-1.76376567086387,1.4057740509142));
#47685=CARTESIAN_POINT('Ctrl Pts',(0.612746020283587,-1.99280368611139,
0.280213560541524));
#47686=CARTESIAN_POINT('Ctrl Pts',(0.589834870344302,-1.91696156463519,
0.652943668424222));
#47687=CARTESIAN_POINT('Ctrl Pts',(0.566485626831716,-1.83962933167279,
1.03297982842434));
#47688=CARTESIAN_POINT('Ctrl Pts',(0.543597158770307,-1.76376567086387,
1.4057740509142));
#47689=CARTESIAN_POINT('',(1.07992491412252,-1.49670618111856,1.4057740509142));
#47690=CARTESIAN_POINT('Origin',(-0.0389049067721117,0.0781315853676385,
1.00012211255832));
#47691=CARTESIAN_POINT('Ctrl Pts',(1.07992491412252,-1.49670618111856,1.4057740509142));
#47692=CARTESIAN_POINT('Ctrl Pts',(1.1266720387397,-1.56068964257619,1.03297982846752));
#47693=CARTESIAN_POINT('Ctrl Pts',(1.174313429993,-1.62592582323378,0.652943668473819));
#47694=CARTESIAN_POINT('Ctrl Pts',(1.22102969697802,-1.68991440488869,0.280213560541524));
#47695=CARTESIAN_POINT('',(-0.148515076362296,-2.07958348927029,0.280213560541524));
#47696=CARTESIAN_POINT('',(0.528108788374353,-2.01688505482942,0.280213560541524));
#47697=CARTESIAN_POINT('Origin',(-0.00909725701023012,0.0981750382072089,
-0.177974371324323));
#47698=CARTESIAN_POINT('',(-0.130256395170145,-1.84103245062609,1.4057740509142));
#47699=CARTESIAN_POINT('Ctrl Pts',(-0.148515076362296,-2.07958348927029,
0.280213560541524));
#47700=CARTESIAN_POINT('Ctrl Pts',(-0.14248860712088,-2.00067609817279,
0.652520236489613));
#47701=CARTESIAN_POINT('Ctrl Pts',(-0.136321810501501,-1.92008267222723,
1.03278544865149));
#47702=CARTESIAN_POINT('Ctrl Pts',(-0.130256395170145,-1.84103245062609,
1.4057740509142));
#47703=CARTESIAN_POINT('',(0.46632735760125,-1.78575082480554,1.4057740509142));
#47704=CARTESIAN_POINT('Origin',(-0.00805336107250954,0.0869096069398723,
1.00012211255832));
#47705=CARTESIAN_POINT('Ctrl Pts',(0.46632735760125,-1.78575082480554,1.4057740509142));
#47706=CARTESIAN_POINT('Ctrl Pts',(0.486814937810489,-1.86234054901206,
1.03278544869513));
#47707=CARTESIAN_POINT('Ctrl Pts',(0.507685736154786,-1.94042857282091,
0.652520236541599));
#47708=CARTESIAN_POINT('Ctrl Pts',(0.528108788374353,-2.01688505482942,
0.280213560541524));
#47709=CARTESIAN_POINT('',(-0.889718388995002,-1.88550401883333,0.280213560541524));
#47710=CARTESIAN_POINT('',(-0.236136138451081,-2.07146420216955,0.280213560541524));
#47711=CARTESIAN_POINT('Origin',(0.0269819748541655,0.0948318050290418,
-0.177974371324323));
#47712=CARTESIAN_POINT('',(-0.786518101167265,-1.66965759641828,1.4057740509142));
#47713=CARTESIAN_POINT('Ctrl Pts',(-0.889718388995002,-1.88550401883333,
0.280213560541524));
#47714=CARTESIAN_POINT('Ctrl Pts',(-0.855578399296262,-1.81406894201494,
0.65269302441041));
#47715=CARTESIAN_POINT('Ctrl Pts',(-0.820724037780499,-1.7411658402745,
1.03285226318453));
#47716=CARTESIAN_POINT('Ctrl Pts',(-0.786518101167265,-1.66965759641828,
1.4057740509142));
#47717=CARTESIAN_POINT('',(-0.210250292573155,-1.83361992441561,1.4057740509142));
#47718=CARTESIAN_POINT('Origin',(0.0238858356651481,0.0839500045121191,
1.00012211255832));
#47719=CARTESIAN_POINT('Ctrl Pts',(-0.210250292573155,-1.83361992441561,
1.4057740509142));
#47720=CARTESIAN_POINT('Ctrl Pts',(-0.218812058596698,-1.91242456387349,
1.0328522632279));
#47721=CARTESIAN_POINT('Ctrl Pts',(-0.227556820710594,-1.9927564871379,
0.652693024461391));
#47722=CARTESIAN_POINT('Ctrl Pts',(-0.236136138451081,-2.07146420216955,
0.280213560541524));
#47723=CARTESIAN_POINT('',(-1.51076030309415,-1.43677678271449,0.280213560541524));
#47724=CARTESIAN_POINT('',(-0.968489571303184,-1.84628063062728,0.280213560541524));
#47725=CARTESIAN_POINT('Origin',(0.0594171415022222,0.0786810111005316,
-0.177974371324324));
#47726=CARTESIAN_POINT('',(-1.3365561793545,-1.27278623192205,1.4057740509142));
#47727=CARTESIAN_POINT('Ctrl Pts',(-1.51076030309415,-1.43677678271449,
0.280213560541524));
#47728=CARTESIAN_POINT('Ctrl Pts',(-1.45306528620204,-1.38244645898933,
0.653049080203456));
#47729=CARTESIAN_POINT('Ctrl Pts',(-1.39425666924037,-1.3270833341075,1.03302896509998));
#47730=CARTESIAN_POINT('Ctrl Pts',(-1.3365561793545,-1.27278623192205,1.4057740509142));
#47731=CARTESIAN_POINT('',(-0.858432475698466,-1.63384849279461,1.4057740509142));
#47732=CARTESIAN_POINT('Origin',(0.0525991179402441,0.0696524887919709,
1.00012211255832));
#47733=CARTESIAN_POINT('Ctrl Pts',(-0.858432475698466,-1.63384849279461,
1.4057740509142));
#47734=CARTESIAN_POINT('Ctrl Pts',(-0.89486633233541,-1.70420541091867,
1.03302896514302));
#47735=CARTESIAN_POINT('Ctrl Pts',(-0.932022263572612,-1.77591988504572,
0.653049080252408));
#47736=CARTESIAN_POINT('Ctrl Pts',(-0.968489571303184,-1.84628063062728,
0.280213560541524));
#47737=CARTESIAN_POINT('',(-1.9277656668486,-0.794004880635056,0.280213560541524));
#47738=CARTESIAN_POINT('',(-1.57004312096482,-1.37174662932466,0.280213560541524));
#47739=CARTESIAN_POINT('Origin',(0.0838276939486571,0.0519039106363612,
-0.177974371324324));
#47740=CARTESIAN_POINT('',(-1.70608493940645,-0.704018034052772,1.4057740509142));
#47741=CARTESIAN_POINT('Ctrl Pts',(-1.9277656668486,-0.794004880635057,
0.280213560541524));
#47742=CARTESIAN_POINT('Ctrl Pts',(-1.85434143822608,-0.764185673242953,
0.653043245509423));
#47743=CARTESIAN_POINT('Ctrl Pts',(-1.77950274741209,-0.733804480193559,
1.03303237733945));
#47744=CARTESIAN_POINT('Ctrl Pts',(-1.70608493940644,-0.704018034052771,
1.4057740509142));
#47745=CARTESIAN_POINT('',(-1.39067859624214,-1.21341676875466,1.4057740509142));
#47746=CARTESIAN_POINT('Origin',(0.0742085978757352,0.045948018502703,1.00012211255832));
#47747=CARTESIAN_POINT('Ctrl Pts',(-1.39067859624214,-1.21341676875466,
1.4057740509142));
#47748=CARTESIAN_POINT('Ctrl Pts',(-1.45006746242559,-1.26586073387978,
1.03303237738257));
#47749=CARTESIAN_POINT('Ctrl Pts',(-1.51062206618193,-1.31931151963234,
0.653043245558453));
#47750=CARTESIAN_POINT('Ctrl Pts',(-1.57004312096482,-1.37174662932466,
0.280213560541524));
#47751=CARTESIAN_POINT('',(-2.08441559517683,-0.0439982196929346,0.280213560541524));
#47752=CARTESIAN_POINT('',(-1.95955364723089,-0.711950644621268,0.280213560541524));
#47753=CARTESIAN_POINT('Origin',(0.0969168518220385,0.0181168994312522,
-0.177974371324323));
#47754=CARTESIAN_POINT('',(-1.84519747464855,-0.040168299586067,1.4057740509142));
#47755=CARTESIAN_POINT('Ctrl Pts',(-2.08441559517683,-0.0439982196929347,
0.280213560541524));
#47756=CARTESIAN_POINT('Ctrl Pts',(-2.00527294760461,-0.0427180698377973,
0.652594621112284));
#47757=CARTESIAN_POINT('Ctrl Pts',(-1.92446479622355,-0.0414225081496093,
1.03281053473744));
#47758=CARTESIAN_POINT('Ctrl Pts',(-1.84519747464855,-0.040168299586067,
1.4057740509142));
#47759=CARTESIAN_POINT('',(-1.7351058663472,-0.629106386319966,1.4057740509142));
#47760=CARTESIAN_POINT('Origin',(0.0857957954640725,0.0160380137078846,
1.00012211255832));
#47761=CARTESIAN_POINT('Ctrl Pts',(-1.7351058663472,-0.629106386319966,
1.4057740509142));
#47762=CARTESIAN_POINT('Ctrl Pts',(-1.80947351479772,-0.656571530981326,
1.03281053478093));
#47763=CARTESIAN_POINT('Ctrl Pts',(-1.88529288273134,-0.684554726931419,
0.652594621163826));
#47764=CARTESIAN_POINT('Ctrl Pts',(-1.95955364723089,-0.711950644621269,
0.280213560541524));
#47765=CARTESIAN_POINT('',(-1.95955364723089,0.711950644621269,0.280213560541524));
#47766=CARTESIAN_POINT('',(-2.08441559517683,0.043998219692935,0.280213560541524));
#47767=CARTESIAN_POINT('Origin',(0.096916851822038,-0.0181168994312522,
-0.177974371324323));
#47768=CARTESIAN_POINT('',(-1.7351058663472,0.629106386319967,1.4057740509142));
#47769=CARTESIAN_POINT('Ctrl Pts',(-1.95955364723089,0.711950644621269,
0.280213560541524));
#47770=CARTESIAN_POINT('Ctrl Pts',(-1.88529288274162,0.684554726935211,
0.652594621112283));
#47771=CARTESIAN_POINT('Ctrl Pts',(-1.80947351480639,0.65657153098453,1.03281053473744));
#47772=CARTESIAN_POINT('Ctrl Pts',(-1.7351058663472,0.629106386319967,1.4057740509142));
#47773=CARTESIAN_POINT('',(-1.84519747464855,0.0401682995860675,1.4057740509142));
#47774=CARTESIAN_POINT('Origin',(0.0857957954640725,-0.0160380137078846,
1.00012211255832));
#47775=CARTESIAN_POINT('Ctrl Pts',(-1.84519747464855,0.0401682995860675,
1.4057740509142));
#47776=CARTESIAN_POINT('Ctrl Pts',(-1.92446479621431,0.0414225081494635,
1.03281053478093));
#47777=CARTESIAN_POINT('Ctrl Pts',(-2.00527294759366,0.0427180698376206,
0.652594621163825));
#47778=CARTESIAN_POINT('Ctrl Pts',(-2.08441559517683,0.0439982196929352,
0.280213560541524));
#47779=CARTESIAN_POINT('',(-1.57004312096482,1.37174662932466,0.280213560541524));
#47780=CARTESIAN_POINT('',(-1.9277656668486,0.794004880635056,0.280213560541524));
#47781=CARTESIAN_POINT('Origin',(0.0838276939486566,-0.0519039106363608,
-0.177974371324323));
#47782=CARTESIAN_POINT('',(-1.39067859624214,1.21341676875466,1.4057740509142));
#47783=CARTESIAN_POINT('Ctrl Pts',(-1.57004312096482,1.37174662932466,0.280213560541524));
#47784=CARTESIAN_POINT('Ctrl Pts',(-1.51062206618974,1.31931151963924,0.653043245509422));
#47785=CARTESIAN_POINT('Ctrl Pts',(-1.45006746243246,1.26586073388585,1.03303237733946));
#47786=CARTESIAN_POINT('Ctrl Pts',(-1.39067859624214,1.21341676875466,1.4057740509142));
#47787=CARTESIAN_POINT('',(-1.70608493940645,0.704018034052771,1.4057740509142));
#47788=CARTESIAN_POINT('Origin',(0.0742085978757352,-0.0459480185027024,
1.00012211255832));
#47789=CARTESIAN_POINT('Ctrl Pts',(-1.70608493940645,0.704018034052771,
1.4057740509142));
#47790=CARTESIAN_POINT('Ctrl Pts',(-1.7795027474036,0.733804480190114,1.03303237738257));
#47791=CARTESIAN_POINT('Ctrl Pts',(-1.85434143821642,0.764185673239031,
0.653043245558453));
#47792=CARTESIAN_POINT('Ctrl Pts',(-1.9277656668486,0.794004880635056,0.280213560541524));
#47793=CARTESIAN_POINT('',(-0.968489571303183,1.84628063062728,0.280213560541524));
#47794=CARTESIAN_POINT('',(-1.51076030309415,1.43677678271449,0.280213560541524));
#47795=CARTESIAN_POINT('Origin',(0.0594171415022222,-0.0786810111005312,
-0.177974371324323));
#47796=CARTESIAN_POINT('',(-0.858432475698465,1.63384849279461,1.4057740509142));
#47797=CARTESIAN_POINT('Ctrl Pts',(-0.968489571303183,1.84628063062729,
0.280213560541524));
#47798=CARTESIAN_POINT('Ctrl Pts',(-0.932022263577399,1.77591988505496,
0.653049080203456));
#47799=CARTESIAN_POINT('Ctrl Pts',(-0.894866332339616,1.7042054109268,1.03302896509998));
#47800=CARTESIAN_POINT('Ctrl Pts',(-0.858432475698465,1.63384849279461,
1.4057740509142));
#47801=CARTESIAN_POINT('',(-1.3365561793545,1.27278623192205,1.4057740509142));
#47802=CARTESIAN_POINT('Origin',(0.0525991179402439,-0.0696524887919705,
1.00012211255832));
#47803=CARTESIAN_POINT('Ctrl Pts',(-1.3365561793545,1.27278623192205,1.4057740509142));
#47804=CARTESIAN_POINT('Ctrl Pts',(-1.3942566692337,1.32708333410123,1.03302896514302));
#47805=CARTESIAN_POINT('Ctrl Pts',(-1.45306528619447,1.3824464589822,0.653049080252408));
#47806=CARTESIAN_POINT('Ctrl Pts',(-1.51076030309415,1.43677678271449,0.280213560541524));
#47807=CARTESIAN_POINT('',(-0.23613613845108,2.07146420216955,0.280213560541524));
#47808=CARTESIAN_POINT('',(-0.889718388995002,1.88550401883333,0.280213560541524));
#47809=CARTESIAN_POINT('Origin',(0.0269819748541655,-0.0948318050290409,
-0.177974371324323));
#47810=CARTESIAN_POINT('',(-0.210250292573154,1.83361992441561,1.4057740509142));
#47811=CARTESIAN_POINT('Ctrl Pts',(-0.236136138451081,2.07146420216955,
0.280213560541524));
#47812=CARTESIAN_POINT('Ctrl Pts',(-0.227556820711768,1.99275648714867,
0.65269302441041));
#47813=CARTESIAN_POINT('Ctrl Pts',(-0.218812058597693,1.91242456388265,
1.03285226318453));
#47814=CARTESIAN_POINT('Ctrl Pts',(-0.210250292573154,1.83361992441561,
1.4057740509142));
#47815=CARTESIAN_POINT('',(-0.786518101167265,1.66965759641828,1.4057740509142));
#47816=CARTESIAN_POINT('Origin',(0.0238858356651483,-0.0839500045121184,
1.00012211255832));
#47817=CARTESIAN_POINT('Ctrl Pts',(-0.786518101167265,1.66965759641828,
1.4057740509142));
#47818=CARTESIAN_POINT('Ctrl Pts',(-0.82072403777652,1.74116584026618,1.0328522632279));
#47819=CARTESIAN_POINT('Ctrl Pts',(-0.855578399291589,1.81406894200517,
0.652693024461392));
#47820=CARTESIAN_POINT('Ctrl Pts',(-0.889718388995002,1.88550401883333,
0.280213560541524));
#47821=CARTESIAN_POINT('',(0.528108788374354,2.01688505482942,0.280213560541524));
#47822=CARTESIAN_POINT('',(-0.148515076362295,2.07958348927029,0.280213560541524));
#47823=CARTESIAN_POINT('Origin',(-0.00909725701022968,-0.0981750382072075,
-0.177974371324323));
#47824=CARTESIAN_POINT('',(0.466327357601251,1.78575082480554,1.4057740509142));
#47825=CARTESIAN_POINT('Ctrl Pts',(0.528108788374354,2.01688505482942,0.280213560541524));
#47826=CARTESIAN_POINT('Ctrl Pts',(0.507685736157639,1.94042857283158,0.652520236489614));
#47827=CARTESIAN_POINT('Ctrl Pts',(0.486814937812886,1.86234054902102,1.03278544865149));
#47828=CARTESIAN_POINT('Ctrl Pts',(0.466327357601251,1.78575082480554,1.40577405091419));
#47829=CARTESIAN_POINT('',(-0.130256395170144,1.84103245062609,1.4057740509142));
#47830=CARTESIAN_POINT('Origin',(-0.00805336107250976,-0.0869096069398716,
1.00012211255832));
#47831=CARTESIAN_POINT('Ctrl Pts',(-0.130256395170144,1.84103245062609,
1.4057740509142));
#47832=CARTESIAN_POINT('Ctrl Pts',(-0.136321810500791,1.92008267221798,
1.03278544869513));
#47833=CARTESIAN_POINT('Ctrl Pts',(-0.142488607120037,2.00067609816177,
0.652520236541599));
#47834=CARTESIAN_POINT('Ctrl Pts',(-0.148515076362295,2.07958348927029,
0.280213560541524));
#47835=CARTESIAN_POINT('',(1.22102969697802,1.68991440488869,0.280213560541524));
#47836=CARTESIAN_POINT('',(0.612746020283587,1.99280368611139,0.280213560541524));
#47837=CARTESIAN_POINT('Origin',(-0.0439478539057538,-0.0882591884688253,
-0.177974371324324));
#47838=CARTESIAN_POINT('',(1.07992491412252,1.49670618111856,1.4057740509142));
#47839=CARTESIAN_POINT('Ctrl Pts',(1.22102969697802,1.68991440488869,0.280213560541524));
#47840=CARTESIAN_POINT('Ctrl Pts',(1.17431342999922,1.6259258232423,0.652943668424222));
#47841=CARTESIAN_POINT('Ctrl Pts',(1.12667203874511,1.5606896425836,1.03297982842434));
#47842=CARTESIAN_POINT('Ctrl Pts',(1.07992491412252,1.49670618111856,1.4057740509142));
#47843=CARTESIAN_POINT('',(0.543597158770306,1.76376567086387,1.4057740509142));
#47844=CARTESIAN_POINT('Origin',(-0.0389049067721121,-0.078131585367639,
1.00012211255832));
#47845=CARTESIAN_POINT('Ctrl Pts',(0.543597158770306,1.76376567086387,1.4057740509142));
#47846=CARTESIAN_POINT('Ctrl Pts',(0.566485626829063,1.839629331664,1.03297982846752));
#47847=CARTESIAN_POINT('Ctrl Pts',(0.589834870341253,1.9169615646251,0.652943668473819));
#47848=CARTESIAN_POINT('Ctrl Pts',(0.612746020283587,1.99280368611139,0.280213560541524));
#47849=CARTESIAN_POINT('',(1.74904377904567,1.13471145042876,0.280213560541524));
#47850=CARTESIAN_POINT('',(1.29125237154726,1.63688470263671,0.280213560541524));
#47851=CARTESIAN_POINT('Origin',(-0.0728630496078391,-0.0664234462666808,
-0.177974371324324));
#47852=CARTESIAN_POINT('',(1.54767262692101,1.00552307413627,1.4057740509142));
#47853=CARTESIAN_POINT('Ctrl Pts',(1.74904377904568,1.13471145042876,0.280213560541524));
#47854=CARTESIAN_POINT('Ctrl Pts',(1.68234743476795,1.09190729901762,0.653052008848806));
#47855=CARTESIAN_POINT('Ctrl Pts',(1.61436802906772,1.04829342427202,1.03302725266642));
#47856=CARTESIAN_POINT('Ctrl Pts',(1.54767262692101,1.00552307413627,1.4057740509142));
#47857=CARTESIAN_POINT('',(1.14403490424299,1.44829256388851,1.4057740509142));
#47858=CARTESIAN_POINT('Origin',(-0.0645021292326093,-0.0588014602494451,
1.00012211255832));
#47859=CARTESIAN_POINT('Ctrl Pts',(1.14403490424299,1.44829256388851,1.4057740509142));
#47860=CARTESIAN_POINT('Ctrl Pts',(1.19277667893946,1.51075710515983,1.03302725270942));
#47861=CARTESIAN_POINT('Ctrl Pts',(1.24247685282478,1.57442234202617,0.653052008897718));
#47862=CARTESIAN_POINT('Ctrl Pts',(1.29125237154726,1.63688470263671,0.280213560541524));
#47863=CARTESIAN_POINT('',(2.04083980696707,0.426259426935219,0.280213560541524));
#47864=CARTESIAN_POINT('',(1.79536793495708,1.0598953697797,0.280213560541524));
#47865=CARTESIAN_POINT('Origin',(-0.0919376867122907,-0.0356168495811993,
-0.177974371324324));
#47866=CARTESIAN_POINT('',(1.80639857550374,0.378538504196172,1.4057740509142));
#47867=CARTESIAN_POINT('Ctrl Pts',(2.04083980696707,0.426259426935219,0.280213560541524));
#47868=CARTESIAN_POINT('Ctrl Pts',(1.96323474208109,0.410449442792685,0.652811627092499));
#47869=CARTESIAN_POINT('Ctrl Pts',(1.88406502084756,0.394332472138682,1.03291010039994));
#47870=CARTESIAN_POINT('Ctrl Pts',(1.80639857550374,0.378538504196172,1.4057740509142));
#47871=CARTESIAN_POINT('',(1.58996439658141,0.937219520893876,1.4057740509142));
#47872=CARTESIAN_POINT('Origin',(-0.0813879817216063,-0.0315298720944253,
1.00012211255832));
#47873=CARTESIAN_POINT('Ctrl Pts',(1.58996439658141,0.937219520893876,1.4057740509142));
#47874=CARTESIAN_POINT('Ctrl Pts',(1.65800091965018,0.977871183626988,1.03291010044321));
#47875=CARTESIAN_POINT('Ctrl Pts',(1.72736598253273,1.01929689489808,0.652811627142823));
#47876=CARTESIAN_POINT('Ctrl Pts',(1.79536793495708,1.0598953697797,0.280213560541524));
#47877=CARTESIAN_POINT('',(1.82116038686464,0.299569788289876,1.4057740509142));
#47878=CARTESIAN_POINT('',(2.05700911027379,0.339761294150944,0.280213560541524));
#47879=CARTESIAN_POINT('Ctrl Pts',(1.82116038686464,0.299569788289876,1.4057740509142));
#47880=CARTESIAN_POINT('Ctrl Pts',(1.89931264504173,0.312902975680572,1.03279071366283));
#47881=CARTESIAN_POINT('Ctrl Pts',(1.97900261625265,0.326481279972747,0.652480914840093));
#47882=CARTESIAN_POINT('Ctrl Pts',(2.05700911027379,0.339761294150944,0.280213560541524));
#47883=CARTESIAN_POINT('',(2.05700911027379,-0.339761294150944,0.280213560541524));
#47884=CARTESIAN_POINT('Origin',(-0.0985956297819381,-4.44089209850063E-16,
-0.177974371324324));
#47885=CARTESIAN_POINT('',(1.82116038686464,-0.299569788289876,1.4057740509142));
#47886=CARTESIAN_POINT('Ctrl Pts',(2.05700911027379,-0.339761294150944,
0.280213560541524));
#47887=CARTESIAN_POINT('Ctrl Pts',(1.97900261626361,-0.326481279974613,
0.652480914787787));
#47888=CARTESIAN_POINT('Ctrl Pts',(1.89931264505091,-0.312902975682139,
1.03279071361899));
#47889=CARTESIAN_POINT('Ctrl Pts',(1.82116038686464,-0.299569788289876,
1.4057740509142));
#47890=CARTESIAN_POINT('Origin',(-0.0872819362927251,-2.22044604925031E-16,
1.00012211255832));
#47891=CARTESIAN_POINT('Origin',(0.,0.,0.194422583515688));
#47892=CARTESIAN_POINT('',(-2.06222171593972,-2.52549322355774E-16,0.194422583515688));
#47893=CARTESIAN_POINT('Origin',(0.,0.,1.4562329884623));
#47894=CARTESIAN_POINT('',(-1.79401563478481,-2.19703550475953E-16,1.4562329884623));
#47895=CARTESIAN_POINT('Origin',(1.68353271183615,-0.652204047184062,1.40243487042194));
#47896=CARTESIAN_POINT('Origin',(1.68353271183615,-0.652204047184062,1.40243487042194));
#47897=CARTESIAN_POINT('Origin',(1.68353271183615,-0.652204047184062,1.40243487042194));
#47898=CARTESIAN_POINT('',(1.42304436641037,-0.516927480140812,1.34041816052587));
#47899=CARTESIAN_POINT('Origin',(1.68353271183615,-0.652204047184062,1.40243487042194));
#47900=CARTESIAN_POINT('',(1.39989426782994,-0.576684772985975,1.34041816052587));
#47901=CARTESIAN_POINT('Origin',(-0.0549728800446225,0.0212966071870162,
1.0061434213025));
#47902=CARTESIAN_POINT('Origin',(1.68353271183615,-0.652204047184062,1.40243487042194));
#47903=CARTESIAN_POINT('Origin',(1.79500904160339,-0.69539020741027,0.84));
#47904=CARTESIAN_POINT('Origin',(1.90648537137062,-0.738576367636477,0.277565129578061));
#47905=CARTESIAN_POINT('Origin',(1.79500904160339,-0.69539020741027,0.84));
#47906=CARTESIAN_POINT('',(1.72523663201451,-0.45673394652411,0.22));
#47907=CARTESIAN_POINT('Origin',(1.90648537137062,-0.738576367636477,0.277565129578061));
#47908=CARTESIAN_POINT('',(1.60754702144021,-0.587633297864109,0.22));
#47909=CARTESIAN_POINT('Origin',(1.92030584968083,-0.743930449457738,0.22));
#47910=CARTESIAN_POINT('Ctrl Pts',(1.42304436641037,-0.516927480140814,
1.34041816052587));
#47911=CARTESIAN_POINT('Ctrl Pts',(1.48410498320936,-0.540267046545479,
0.969742401437925));
#47912=CARTESIAN_POINT('Ctrl Pts',(1.54648225040979,-0.564172784216683,
0.59094512501486));
#47913=CARTESIAN_POINT('Ctrl Pts',(1.60754702144021,-0.587633297864117,
0.22));
#47914=CARTESIAN_POINT('Origin',(2.21659783251117,-0.858714575118933,0.3482551044561));
#47915=CARTESIAN_POINT('Origin',(1.33424422438224,-1.21632432380853,1.40243487042194));
#47916=CARTESIAN_POINT('Origin',(1.33424422438224,-1.21632432380853,1.40243487042194));
#47917=CARTESIAN_POINT('Origin',(1.33424422438224,-1.21632432380853,1.40243487042194));
#47918=CARTESIAN_POINT('',(1.14021360866399,-0.996083437827601,1.34041816052587));
#47919=CARTESIAN_POINT('Origin',(1.33424422438224,-1.21632432380853,1.40243487042194));
#47920=CARTESIAN_POINT('',(1.09703996059555,-1.04344267372651,1.34041816052587));
#47921=CARTESIAN_POINT('Origin',(-0.0435674621476161,0.0397169895648517,
1.0061434213025));
#47922=CARTESIAN_POINT('Origin',(1.33424422438224,-1.21632432380853,1.40243487042194));
#47923=CARTESIAN_POINT('Origin',(1.42259216564977,-1.29686411401962,0.84));
#47924=CARTESIAN_POINT('Origin',(1.5109401069173,-1.37740390423071,0.277565129578061));
#47925=CARTESIAN_POINT('Origin',(1.42259216564977,-1.29686411401962,0.84));
#47926=CARTESIAN_POINT('',(1.44374391665803,-1.04911907687602,0.22));
#47927=CARTESIAN_POINT('Origin',(1.5109401069173,-1.37740390423071,0.277565129578061));
#47928=CARTESIAN_POINT('',(1.2867153233272,-1.12866469583084,0.22));
#47929=CARTESIAN_POINT('Origin',(1.52189320170064,-1.38738896945528,0.22));
#47930=CARTESIAN_POINT('Ctrl Pts',(1.14021360866399,-0.996083437827602,
1.34041816052587));
#47931=CARTESIAN_POINT('Ctrl Pts',(1.18866923103111,-1.03985896697717,0.970128186228657));
#47932=CARTESIAN_POINT('Ctrl Pts',(1.23815819319504,-1.08464692910743,0.591640399915973));
#47933=CARTESIAN_POINT('Ctrl Pts',(1.2867153233272,-1.12866469583084,0.22));
#47934=CARTESIAN_POINT('Origin',(1.75671243867939,-1.60145498856633,0.3482551044561));
#47935=CARTESIAN_POINT('Origin',(0.804758661123036,-1.61617326061691,1.40243487042194));
#47936=CARTESIAN_POINT('Origin',(0.804758661123036,-1.61617326061691,1.40243487042194));
#47937=CARTESIAN_POINT('Origin',(0.804758661123036,-1.61617326061691,1.40243487042194));
#47938=CARTESIAN_POINT('',(0.703390684925828,-1.3407128077469,1.34041816052587));
#47939=CARTESIAN_POINT('Origin',(0.804758661123036,-1.61617326061691,1.40243487042194));
#47940=CARTESIAN_POINT('',(0.646024327774458,-1.36927785946482,1.34041816052587));
#47941=CARTESIAN_POINT('Origin',(-0.0262780170719328,0.0527733724225172,
1.0061434213025));
#47942=CARTESIAN_POINT('Origin',(0.804758661123036,-1.61617326061691,1.40243487042194));
#47943=CARTESIAN_POINT('Origin',(0.858046334869837,-1.72318933585849,0.84));
#47944=CARTESIAN_POINT('Origin',(0.911334008616638,-1.83020541110008,0.277565129578061));
#47945=CARTESIAN_POINT('Origin',(0.858046334869837,-1.72318933585849,0.84));
#47946=CARTESIAN_POINT('',(0.967265585295667,-1.49981486252633,0.22));
#47947=CARTESIAN_POINT('Origin',(0.911334008616638,-1.83020541110008,0.277565129578061));
#47948=CARTESIAN_POINT('',(0.792105590863112,-1.51726367247863,0.22));
#47949=CARTESIAN_POINT('Origin',(0.917940443729429,-1.84347292134022,0.22));
#47950=CARTESIAN_POINT('Ctrl Pts',(0.703390684925826,-1.34071280774691,
1.34041816052587));
#47951=CARTESIAN_POINT('Ctrl Pts',(0.732784340667834,-1.39908348436706,
0.969829651658146));
#47952=CARTESIAN_POINT('Ctrl Pts',(0.762770120360982,-1.45876053753165,
0.591113455185774));
#47953=CARTESIAN_POINT('Ctrl Pts',(0.792105590863111,-1.51726367247863,
0.22));
#47954=CARTESIAN_POINT('Origin',(1.05957329572431,-2.12791003183941,0.3482551044561));
#47955=CARTESIAN_POINT('Origin',(0.166585981357483,-1.79774904305379,1.40243487042194));
#47956=CARTESIAN_POINT('Origin',(0.166585981357483,-1.79774904305379,1.40243487042194));
#47957=CARTESIAN_POINT('Origin',(0.166585981357483,-1.79774904305379,1.40243487042194));
#47958=CARTESIAN_POINT('',(0.171570951566094,-1.50427148383386,1.34041816052587));
#47959=CARTESIAN_POINT('Origin',(0.166585981357483,-1.79774904305379,1.40243487042194));
#47960=CARTESIAN_POINT('',(0.107759529743047,-1.51018448285187,1.34041816052587));
#47961=CARTESIAN_POINT('Origin',(-0.00543958017916557,0.0587024189071708,
1.0061434213025));
#47962=CARTESIAN_POINT('Origin',(0.166585981357483,-1.79774904305379,1.40243487042194));
#47963=CARTESIAN_POINT('Origin',(0.177616591966855,-1.91678828936794,0.84));
#47964=CARTESIAN_POINT('Origin',(0.188647202576228,-2.0358275356821,0.277565129578061));
#47965=CARTESIAN_POINT('Origin',(0.177616591966855,-1.91678828936794,0.84));
#47966=CARTESIAN_POINT('',(0.36015267683549,-1.74795234023142,0.22));
#47967=CARTESIAN_POINT('Origin',(0.188647202576228,-2.0358275356821,0.277565129578061));
#47968=CARTESIAN_POINT('',(0.190517609144359,-1.70094778270994,0.22));
#47969=CARTESIAN_POINT('Origin',(0.190014742348963,-2.05058564016207,0.22));
#47970=CARTESIAN_POINT('Ctrl Pts',(0.171570951566093,-1.50427148383386,
1.34041816052587));
#47971=CARTESIAN_POINT('Ctrl Pts',(0.177897879678585,-1.56936071475471,
0.969590466476621));
#47972=CARTESIAN_POINT('Ctrl Pts',(0.184305736125241,-1.63589092068322,
0.590584376399643));
#47973=CARTESIAN_POINT('Ctrl Pts',(0.190517609144358,-1.70094778270994,
0.22));
#47974=CARTESIAN_POINT('Origin',(0.219332907883337,-2.36697903415605,0.3482551044561));
#47975=CARTESIAN_POINT('Origin',(-0.494085058275185,-1.73652885555491,1.40243487042194));
#47976=CARTESIAN_POINT('Origin',(-0.494085058275185,-1.73652885555491,1.40243487042194));
#47977=CARTESIAN_POINT('Origin',(-0.494085058275185,-1.73652885555491,1.40243487042194));
#47978=CARTESIAN_POINT('',(-0.383420389510102,-1.46466996057301,1.34041816052587));
#47979=CARTESIAN_POINT('Origin',(-0.494085058275185,-1.73652885555491,1.40243487042194));
#47980=CARTESIAN_POINT('',(-0.445058789896328,-1.44713232360867,1.34041816052587));
#47981=CARTESIAN_POINT('Origin',(0.0161335021585525,0.0567033784370783,
1.0061434213025));
#47982=CARTESIAN_POINT('Origin',(-0.494085058275185,-1.73652885555491,1.40243487042194));
#47983=CARTESIAN_POINT('Origin',(-0.52680125588876,-1.85151436310768,0.84));
#47984=CARTESIAN_POINT('Origin',(-0.559517453502335,-1.96649987066044,0.277565129578061));
#47985=CARTESIAN_POINT('Origin',(-0.52680125588876,-1.85151436310768,0.84));
#47986=CARTESIAN_POINT('',(-0.295600846306194,-1.76001916864997,0.22));
#47987=CARTESIAN_POINT('Origin',(-0.559517453502335,-1.96649987066044,0.277565129578061));
#47988=CARTESIAN_POINT('',(-0.436800831383855,-1.65490946960924,0.22));
#47989=CARTESIAN_POINT('Origin',(-0.563573502893763,-1.98075540559274,0.22));
#47990=CARTESIAN_POINT('Ctrl Pts',(-0.383420389510103,-1.46466996057301,
1.34041816052587));
#47991=CARTESIAN_POINT('Ctrl Pts',(-0.401029817090961,-1.5276357164313,
0.96967110048816));
#47992=CARTESIAN_POINT('Ctrl Pts',(-0.419081848799302,-1.59196577132107,
0.590796412809183));
#47993=CARTESIAN_POINT('Ctrl Pts',(-0.436800831383856,-1.65490946960923,
0.22));
#47994=CARTESIAN_POINT('Origin',(-0.650529604532875,-2.28637440202631,0.3482551044561));
#47995=CARTESIAN_POINT('Origin',(-1.08802717296797,-1.44078082367478,1.40243487042194));
#47996=CARTESIAN_POINT('Origin',(-1.08802717296797,-1.44078082367478,1.40243487042194));
#47997=CARTESIAN_POINT('Origin',(-1.08802717296797,-1.44078082367478,1.40243487042194));
#47998=CARTESIAN_POINT('',(-0.886628682377235,-1.22725664312035,1.34041816052587));
#47999=CARTESIAN_POINT('Origin',(-1.08802717296797,-1.44078082367478,1.40243487042194));
#48000=CARTESIAN_POINT('',(-0.937769453804317,-1.18863692522509,1.34041816052587));
#48001=CARTESIAN_POINT('Origin',(0.0355276656309362,0.0470462325047916,
1.0061434213025));
#48002=CARTESIAN_POINT('Origin',(-1.08802717296797,-1.44078082367478,1.40243487042194));
#48003=CARTESIAN_POINT('Origin',(-1.16007167503007,-1.53618316251446,0.84));
#48004=CARTESIAN_POINT('Origin',(-1.23211617709217,-1.63158550135414,0.277565129578061));
#48005=CARTESIAN_POINT('Origin',(-1.16007167503007,-1.53618316251446,0.84));
#48006=CARTESIAN_POINT('',(-0.911431837173392,-1.53438565573945,0.22));
#48007=CARTESIAN_POINT('Origin',(-1.23211617709217,-1.63158550135414,0.277565129578061));
#48008=CARTESIAN_POINT('',(-1.00512689923672,-1.38536646246786,0.22));
#48009=CARTESIAN_POINT('Origin',(-1.2410480237021,-1.64341317775352,0.22));
#48010=CARTESIAN_POINT('Ctrl Pts',(-0.886628682377236,-1.22725664312035,
1.34041816052587));
#48011=CARTESIAN_POINT('Ctrl Pts',(-0.92575705730228,-1.27955870074339,
0.970028743491965));
#48012=CARTESIAN_POINT('Ctrl Pts',(-0.965795109999248,-1.33297888801976,
0.591471165657163));
#48013=CARTESIAN_POINT('Ctrl Pts',(-1.00512689923672,-1.38536646246787,
0.22));
#48014=CARTESIAN_POINT('Origin',(-1.43253448914795,-1.896982237665,0.3482551044561));
#48015=CARTESIAN_POINT('Origin',(-1.53502518898474,-0.950447357915218,1.40243487042194));
#48016=CARTESIAN_POINT('Origin',(-1.53502518898474,-0.950447357915218,1.40243487042194));
#48017=CARTESIAN_POINT('Origin',(-1.53502518898474,-0.950447357915218,1.40243487042194));
#48018=CARTESIAN_POINT('',(-1.27009285871019,-0.824095515550463,1.34041816052587));
#48019=CARTESIAN_POINT('Origin',(-1.53502518898474,-0.950447357915218,1.40243487042194));
#48020=CARTESIAN_POINT('',(-1.3038291566161,-0.769609523625294,1.34041816052587));
#48021=CARTESIAN_POINT('Origin',(0.0501236209942708,0.0310352321805594,
1.0061434213025));
#48022=CARTESIAN_POINT('Origin',(-1.53502518898474,-0.950447357915218,1.40243487042194));
#48023=CARTESIAN_POINT('Origin',(-1.63666798627951,-1.01338191353891,0.84));
#48024=CARTESIAN_POINT('Origin',(-1.73831078357428,-1.0763164691626,0.277565129578061));
#48025=CARTESIAN_POINT('Origin',(-1.63666798627951,-1.01338191353891,0.84));
#48026=CARTESIAN_POINT('',(-1.40416890801217,-1.1015248576969,0.22));
#48027=CARTESIAN_POINT('Origin',(-1.73831078357428,-1.0763164691626,0.277565129578061));
#48028=CARTESIAN_POINT('',(-1.43770500974724,-0.928722037989642,0.22));
#48029=CARTESIAN_POINT('Origin',(-1.75091213202498,-1.0841188937919,0.22));
#48030=CARTESIAN_POINT('Ctrl Pts',(-1.27009285871019,-0.824095515550462,
1.34041816052587));
#48031=CARTESIAN_POINT('Ctrl Pts',(-1.32548789695821,-0.85874045931348,
0.969926863920483));
#48032=CARTESIAN_POINT('Ctrl Pts',(-1.38213150089445,-0.894097100162996,
0.591291664620299));
#48033=CARTESIAN_POINT('Ctrl Pts',(-1.43770500974724,-0.928722037989639,
0.22));
#48034=CARTESIAN_POINT('Origin',(-2.02106765305595,-1.25139211056558,0.3482551044561));
#48035=CARTESIAN_POINT('Origin',(-1.77470954736091,-0.331750709858588,1.40243487042194));
#48036=CARTESIAN_POINT('Origin',(-1.77470954736091,-0.331750709858588,1.40243487042194));
#48037=CARTESIAN_POINT('Origin',(-1.77470954736091,-0.331750709858588,1.40243487042194));
#48038=CARTESIAN_POINT('',(-1.48202395664685,-0.309635722134599,1.34041816052587));
#48039=CARTESIAN_POINT('Origin',(-1.77470954736091,-0.331750709858588,1.40243487042194));
#48040=CARTESIAN_POINT('',(-1.49379950706012,-0.246642091306309,1.34041816052587));
#48041=CARTESIAN_POINT('Origin',(0.0579501035977568,0.0108327517781841,
1.0061434213025));
#48042=CARTESIAN_POINT('Origin',(-1.77470954736091,-0.331750709858588,1.40243487042194));
#48043=CARTESIAN_POINT('Origin',(-1.89222321689151,-0.353717821796897,0.84));
#48044=CARTESIAN_POINT('Origin',(-2.00973688642211,-0.375684933735207,0.277565129578061));
#48045=CARTESIAN_POINT('Origin',(-1.89222321689151,-0.353717821796897,0.84));
#48046=CARTESIAN_POINT('',(-1.70726518705538,-0.519897023862431,0.22));
#48047=CARTESIAN_POINT('Origin',(-2.00973688642211,-0.375684933735207,0.277565129578061));
#48048=CARTESIAN_POINT('',(-1.67611309209292,-0.346648556054458,0.22));
#48049=CARTESIAN_POINT('Origin',(-2.02430585477882,-0.378408345913518,0.22));
#48050=CARTESIAN_POINT('Ctrl Pts',(-1.48202395664686,-0.309635722134596,
1.34041816052587));
#48051=CARTESIAN_POINT('Ctrl Pts',(-1.54624662587943,-0.32194035490071,
0.96962006919933));
#48052=CARTESIAN_POINT('Ctrl Pts',(-1.61189130995875,-0.334457530455581,
0.59067441941184));
#48053=CARTESIAN_POINT('Ctrl Pts',(-1.67611309209293,-0.346648556054445,
0.22));
#48054=CARTESIAN_POINT('Origin',(-2.33664443129628,-0.43679454473122,0.3482551044561));
#48055=CARTESIAN_POINT('Origin',(-1.77470954736091,0.331750709858588,1.40243487042194));
#48056=CARTESIAN_POINT('Origin',(-1.77470954736091,0.331750709858588,1.40243487042194));
#48057=CARTESIAN_POINT('Origin',(-1.77470954736091,0.331750709858588,1.40243487042194));
#48058=CARTESIAN_POINT('',(-1.49379950706012,0.24664209130631,1.34041816052587));
#48059=CARTESIAN_POINT('Origin',(-1.77470954736091,0.331750709858588,1.40243487042194));
#48060=CARTESIAN_POINT('',(-1.48202395664685,0.309635722134599,1.34041816052587));
#48061=CARTESIAN_POINT('Origin',(0.0579501035977565,-0.0108327517781845,
1.0061434213025));
#48062=CARTESIAN_POINT('Origin',(-1.77470954736091,0.331750709858588,1.40243487042194));
#48063=CARTESIAN_POINT('Origin',(-1.89222321689151,0.353717821796898,0.84));
#48064=CARTESIAN_POINT('Origin',(-2.00973688642211,0.375684933735208,0.277565129578061));
#48065=CARTESIAN_POINT('Origin',(-1.89222321689151,0.353717821796898,0.84));
#48066=CARTESIAN_POINT('',(-1.77978584230378,0.131945783893516,0.22));
#48067=CARTESIAN_POINT('Origin',(-2.00973688642211,0.375684933735208,0.277565129578061));
#48068=CARTESIAN_POINT('',(-1.6881528136882,0.282241734221853,0.22));
#48069=CARTESIAN_POINT('Origin',(-2.02430585477882,0.378408345913518,0.22));
#48070=CARTESIAN_POINT('Ctrl Pts',(-1.49379950706012,0.246642091306312,
1.34041816052587));
#48071=CARTESIAN_POINT('Ctrl Pts',(-1.55813030865998,0.258368266999456,
0.96962006919933));
#48072=CARTESIAN_POINT('Ctrl Pts',(-1.62386387892535,0.270409943457099,
0.59067441941184));
#48073=CARTESIAN_POINT('Ctrl Pts',(-1.6881528136882,0.282241734221861,0.22));
#48074=CARTESIAN_POINT('Origin',(-2.33664443129628,0.43679454473122,0.3482551044561));
#48075=CARTESIAN_POINT('Origin',(-1.53502518898474,0.950447357915218,1.40243487042194));
#48076=CARTESIAN_POINT('Origin',(-1.53502518898474,0.950447357915218,1.40243487042194));
#48077=CARTESIAN_POINT('Origin',(-1.53502518898474,0.950447357915218,1.40243487042194));
#48078=CARTESIAN_POINT('',(-1.3038291566161,0.769609523625295,1.34041816052587));
#48079=CARTESIAN_POINT('Origin',(-1.53502518898474,0.950447357915218,1.40243487042194));
#48080=CARTESIAN_POINT('',(-1.27009285871019,0.824095515550462,1.34041816052587));
#48081=CARTESIAN_POINT('Origin',(0.0501236209942704,-0.0310352321805596,
1.0061434213025));
#48082=CARTESIAN_POINT('Origin',(-1.53502518898474,0.950447357915218,1.40243487042194));
#48083=CARTESIAN_POINT('Origin',(-1.63666798627951,1.01338191353891,0.84));
#48084=CARTESIAN_POINT('Origin',(-1.73831078357428,1.0763164691626,0.277565129578061));
#48085=CARTESIAN_POINT('Origin',(-1.63666798627951,1.01338191353891,0.84));
#48086=CARTESIAN_POINT('',(-1.61193655741525,0.765968582397815,0.22));
#48087=CARTESIAN_POINT('Origin',(-1.73831078357428,1.0763164691626,0.277565129578061));
#48088=CARTESIAN_POINT('',(-1.47219814341721,0.873013714336073,0.22));
#48089=CARTESIAN_POINT('Origin',(-1.75091213202497,1.0841188937919,0.22));
#48090=CARTESIAN_POINT('Ctrl Pts',(-1.3038291566161,0.769609523625296,1.34041816052587));
#48091=CARTESIAN_POINT('Ctrl Pts',(-1.35953373177067,0.803754548119228,
0.969926863920484));
#48092=CARTESIAN_POINT('Ctrl Pts',(-1.41643192564858,0.838700012094964,
0.591291664620299));
#48093=CARTESIAN_POINT('Ctrl Pts',(-1.47219814341721,0.873013714336066,
0.22));
#48094=CARTESIAN_POINT('Origin',(-2.02106765305595,1.25139211056558,0.3482551044561));
#48095=CARTESIAN_POINT('Origin',(-1.08802717296797,1.44078082367478,1.40243487042194));
#48096=CARTESIAN_POINT('Origin',(-1.08802717296797,1.44078082367478,1.40243487042194));
#48097=CARTESIAN_POINT('Origin',(-1.08802717296797,1.44078082367478,1.40243487042194));
#48098=CARTESIAN_POINT('',(-0.937769453804316,1.1886369252251,1.34041816052587));
#48099=CARTESIAN_POINT('Origin',(-1.08802717296797,1.44078082367478,1.40243487042194));
#48100=CARTESIAN_POINT('',(-0.886628682377236,1.22725664312035,1.34041816052587));
#48101=CARTESIAN_POINT('Origin',(0.0355276656309362,-0.0470462325047913,
1.0061434213025));
#48102=CARTESIAN_POINT('Origin',(-1.08802717296797,1.44078082367478,1.40243487042194));
#48103=CARTESIAN_POINT('Origin',(-1.16007167503007,1.53618316251446,0.84));
#48104=CARTESIAN_POINT('Origin',(-1.23211617709217,1.63158550135414,0.277565129578061));
#48105=CARTESIAN_POINT('Origin',(-1.16007167503007,1.53618316251446,0.84));
#48106=CARTESIAN_POINT('',(-1.22638630839898,1.29654307947085,0.22));
#48107=CARTESIAN_POINT('Origin',(-1.23211617709217,1.63158550135414,0.277565129578061));
#48108=CARTESIAN_POINT('',(-1.0574149561462,1.3458803547932,0.22));
#48109=CARTESIAN_POINT('Origin',(-1.2410480237021,1.64341317775352,0.22));
#48110=CARTESIAN_POINT('Ctrl Pts',(-0.937769453804315,1.1886369252251,1.34041816052587));
#48111=CARTESIAN_POINT('Ctrl Pts',(-0.977366925938209,1.24058473707973,
0.970028743491965));
#48112=CARTESIAN_POINT('Ctrl Pts',(-1.01779089870601,1.29371349104664,0.591471165657163));
#48113=CARTESIAN_POINT('Ctrl Pts',(-1.05741495614621,1.3458803547932,0.22));
#48114=CARTESIAN_POINT('Origin',(-1.43253448914794,1.896982237665,0.3482551044561));
#48115=CARTESIAN_POINT('Origin',(-0.494085058275185,1.73652885555491,1.40243487042194));
#48116=CARTESIAN_POINT('Origin',(-0.494085058275185,1.73652885555491,1.40243487042194));
#48117=CARTESIAN_POINT('Origin',(-0.494085058275185,1.73652885555491,1.40243487042194));
#48118=CARTESIAN_POINT('',(-0.445058789896327,1.44713232360867,1.34041816052587));
#48119=CARTESIAN_POINT('Origin',(-0.494085058275185,1.73652885555491,1.40243487042194));
#48120=CARTESIAN_POINT('',(-0.383420389510103,1.46466996057301,1.34041816052587));
#48121=CARTESIAN_POINT('Origin',(0.0161335021585525,-0.0567033784370781,
1.0061434213025));
#48122=CARTESIAN_POINT('Origin',(-0.494085058275185,1.73652885555491,1.40243487042194));
#48123=CARTESIAN_POINT('Origin',(-0.52680125588876,1.85151436310768,0.84));
#48124=CARTESIAN_POINT('Origin',(-0.559517453502335,1.96649987066044,0.277565129578062));
#48125=CARTESIAN_POINT('Origin',(-0.52680125588876,1.85151436310768,0.84));
#48126=CARTESIAN_POINT('',(-0.675205792792306,1.65201224926814,0.22));
#48127=CARTESIAN_POINT('Origin',(-0.559517453502335,1.96649987066044,0.277565129578062));
#48128=CARTESIAN_POINT('',(-0.499822019709113,1.63697839555501,0.22));
#48129=CARTESIAN_POINT('Origin',(-0.563573502893763,1.98075540559275,0.22));
#48130=CARTESIAN_POINT('Ctrl Pts',(-0.445058789896326,1.44713232360867,
1.34041816052587));
#48131=CARTESIAN_POINT('Ctrl Pts',(-0.463234151860379,1.50993705725198,
0.969671100488159));
#48132=CARTESIAN_POINT('Ctrl Pts',(-0.481751415100855,1.57413474235824,
0.590796412809184));
#48133=CARTESIAN_POINT('Ctrl Pts',(-0.499822019709111,1.63697839555501,
0.22));
#48134=CARTESIAN_POINT('Origin',(-0.650529604532875,2.28637440202631,0.3482551044561));
#48135=CARTESIAN_POINT('Origin',(0.166585981357484,1.79774904305379,1.40243487042194));
#48136=CARTESIAN_POINT('Origin',(0.166585981357484,1.79774904305379,1.40243487042194));
#48137=CARTESIAN_POINT('Origin',(0.166585981357484,1.79774904305379,1.40243487042194));
#48138=CARTESIAN_POINT('',(0.107759529743047,1.51018448285187,1.34041816052587));
#48139=CARTESIAN_POINT('Origin',(0.166585981357484,1.79774904305379,1.40243487042194));
#48140=CARTESIAN_POINT('',(0.171570951566095,1.50427148383386,1.34041816052587));
#48141=CARTESIAN_POINT('Origin',(-0.00543958017916535,-0.0587024189071703,
1.0061434213025));
#48142=CARTESIAN_POINT('Origin',(0.166585981357484,1.79774904305379,1.40243487042194));
#48143=CARTESIAN_POINT('Origin',(0.177616591966856,1.91678828936794,0.84));
#48144=CARTESIAN_POINT('Origin',(0.188647202576229,2.0358275356821,0.277565129578061));
#48145=CARTESIAN_POINT('Origin',(0.177616591966856,1.91678828936794,0.84));
#48146=CARTESIAN_POINT('',(-0.0328349934245687,1.78436801068587,0.22));
#48147=CARTESIAN_POINT('Origin',(0.188647202576229,2.0358275356821,0.277565129578061));
#48148=CARTESIAN_POINT('',(0.12527465009912,1.70699343318669,0.22));
#48149=CARTESIAN_POINT('Origin',(0.190014742348964,2.05058564016207,0.22));
#48150=CARTESIAN_POINT('Ctrl Pts',(0.107759529743049,1.51018448285187,1.34041816052587));
#48151=CARTESIAN_POINT('Ctrl Pts',(0.113500444401593,1.57532801591611,0.96959046647662));
#48152=CARTESIAN_POINT('Ctrl Pts',(0.119426587147494,1.64190285919258,0.590584376399643));
#48153=CARTESIAN_POINT('Ctrl Pts',(0.12527465009912,1.70699343318669,0.22));
#48154=CARTESIAN_POINT('Origin',(0.219332907883338,2.36697903415605,0.3482551044561));
#48155=CARTESIAN_POINT('Origin',(0.804758661123035,1.61617326061691,1.40243487042194));
#48156=CARTESIAN_POINT('Origin',(0.804758661123035,1.61617326061691,1.40243487042194));
#48157=CARTESIAN_POINT('Origin',(0.804758661123035,1.61617326061691,1.40243487042194));
#48158=CARTESIAN_POINT('',(0.646024327774458,1.36927785946482,1.34041816052587));
#48159=CARTESIAN_POINT('Origin',(0.804758661123035,1.61617326061691,1.40243487042194));
#48160=CARTESIAN_POINT('',(0.703390684925827,1.3407128077469,1.34041816052587));
#48161=CARTESIAN_POINT('Origin',(-0.0262780170719323,-0.052773372422517,
1.0061434213025));
#48162=CARTESIAN_POINT('Origin',(0.804758661123035,1.61617326061691,1.40243487042194));
#48163=CARTESIAN_POINT('Origin',(0.858046334869836,1.7231893358585,0.84));
#48164=CARTESIAN_POINT('Origin',(0.911334008616637,1.83020541110008,0.277565129578061));
#48165=CARTESIAN_POINT('Origin',(0.858046334869836,1.7231893358585,0.84));
#48166=CARTESIAN_POINT('',(0.613970353750136,1.67573498473601,0.22));
#48167=CARTESIAN_POINT('Origin',(0.911334008616637,1.83020541110008,0.277565129578061));
#48168=CARTESIAN_POINT('',(0.733452284240665,1.54646954888937,0.22));
#48169=CARTESIAN_POINT('Origin',(0.917940443729428,1.84347292134022,0.22));
#48170=CARTESIAN_POINT('Ctrl Pts',(0.64602432777446,1.36927785946482,1.34041816052587));
#48171=CARTESIAN_POINT('Ctrl Pts',(0.674891498245406,1.42791069459989,0.969829651658146));
#48172=CARTESIAN_POINT('Ctrl Pts',(0.704444345302139,1.48780332260248,0.591113455185774));
#48173=CARTESIAN_POINT('Ctrl Pts',(0.733452284240667,1.54646954888937,0.22));
#48174=CARTESIAN_POINT('Origin',(1.05957329572431,2.12791003183941,0.3482551044561));
#48175=CARTESIAN_POINT('Origin',(1.33424422438224,1.21632432380853,1.40243487042194));
#48176=CARTESIAN_POINT('Origin',(1.33424422438224,1.21632432380853,1.40243487042194));
#48177=CARTESIAN_POINT('Origin',(1.33424422438224,1.21632432380853,1.40243487042194));
#48178=CARTESIAN_POINT('',(1.09703996059555,1.04344267372651,1.34041816052587));
#48179=CARTESIAN_POINT('Origin',(1.33424422438224,1.21632432380853,1.40243487042194));
#48180=CARTESIAN_POINT('',(1.14021360866399,0.996083437827603,1.34041816052587));
#48181=CARTESIAN_POINT('Origin',(-0.0435674621476159,-0.0397169895648515,
1.0061434213025));
#48182=CARTESIAN_POINT('Origin',(1.33424422438224,1.21632432380853,1.40243487042194));
#48183=CARTESIAN_POINT('Origin',(1.42259216564977,1.29686411401962,0.84));
#48184=CARTESIAN_POINT('Origin',(1.5109401069173,1.37740390423071,0.277565129578062));
#48185=CARTESIAN_POINT('Origin',(1.42259216564977,1.29686411401962,0.84));
#48186=CARTESIAN_POINT('',(1.17785560252371,1.34078466352944,0.22));
#48187=CARTESIAN_POINT('Origin',(1.5109401069173,1.37740390423071,0.277565129578062));
#48188=CARTESIAN_POINT('',(1.2425731231961,1.17708638273095,0.22));
#48189=CARTESIAN_POINT('Origin',(1.52189320170064,1.38738896945528,0.22));
#48190=CARTESIAN_POINT('Ctrl Pts',(1.09703996059555,1.04344267372651,1.34041816052587));
#48191=CARTESIAN_POINT('Ctrl Pts',(1.14509967248684,1.08765249728891,0.970128181227685));
#48192=CARTESIAN_POINT('Ctrl Pts',(1.194262842832,1.1327978368539,0.591640391729911));
#48193=CARTESIAN_POINT('Ctrl Pts',(1.2425731231961,1.17708638273095,0.22));
#48194=CARTESIAN_POINT('Origin',(1.75671243867939,1.60145498856633,0.3482551044561));
#48195=CARTESIAN_POINT('Origin',(1.68353271183615,0.652204047184062,1.40243487042194));
#48196=CARTESIAN_POINT('Origin',(1.68353271183615,0.652204047184062,1.40243487042194));
#48197=CARTESIAN_POINT('Origin',(1.68353271183615,0.652204047184062,1.40243487042194));
#48198=CARTESIAN_POINT('',(1.39989426782994,0.576684772985975,1.34041816052587));
#48199=CARTESIAN_POINT('Origin',(1.68353271183615,0.652204047184062,1.40243487042194));
#48200=CARTESIAN_POINT('',(1.42304436641037,0.516927480140812,1.34041816052587));
#48201=CARTESIAN_POINT('Origin',(-0.0549728800446225,-0.0212966071870164,
1.0061434213025));
#48202=CARTESIAN_POINT('Origin',(1.68353271183615,0.652204047184062,1.40243487042194));
#48203=CARTESIAN_POINT('Origin',(1.79500904160339,0.695390207410269,0.84));
#48204=CARTESIAN_POINT('Origin',(1.90648537137062,0.738576367636477,0.277565129578061));
#48205=CARTESIAN_POINT('Origin',(1.79500904160339,0.695390207410269,0.84));
#48206=CARTESIAN_POINT('',(1.58266492545325,0.824753943968932,0.22));
#48207=CARTESIAN_POINT('Origin',(1.90648537137062,0.738576367636477,0.277565129578061));
#48208=CARTESIAN_POINT('',(1.58387757652854,0.648731178123911,0.22));
#48209=CARTESIAN_POINT('Origin',(1.92030584968083,0.743930449457738,0.22));
#48210=CARTESIAN_POINT('Ctrl Pts',(1.39989426782994,0.576684772985972,1.34041816052587));
#48211=CARTESIAN_POINT('Ctrl Pts',(1.46074237398106,0.6005728974663,0.969742391482374));
#48212=CARTESIAN_POINT('Ctrl Pts',(1.52294492302307,0.624929637725966,0.590945108845491));
#48213=CARTESIAN_POINT('Ctrl Pts',(1.58387757652854,0.648731178123902,0.22));
#48214=CARTESIAN_POINT('Origin',(2.21659783251117,0.858714575118932,0.3482551044561));
#48215=CARTESIAN_POINT('Origin',(2.37711940646971,0.,0.3482551044561));
#48216=CARTESIAN_POINT('Origin',(2.04454922222021,0.,0.277565129578061));
#48217=CARTESIAN_POINT('Origin',(1.80545077777979,0.,1.40243487042194));
#48218=CARTESIAN_POINT('Origin',(1.80545077777979,0.,1.40243487042194));
#48219=CARTESIAN_POINT('Origin',(1.80545077777979,0.,1.40243487042194));
#48220=CARTESIAN_POINT('',(1.51368509711198,0.0320423981330441,1.34041816052587));
#48221=CARTESIAN_POINT('Origin',(1.80545077777979,0.,1.40243487042194));
#48222=CARTESIAN_POINT('',(1.51368509711198,-0.0320423981330441,1.34041816052587));
#48223=CARTESIAN_POINT('Origin',(-0.058953905876358,2.22044604925031E-16,
1.0061434213025));
#48224=CARTESIAN_POINT('Origin',(1.80545077777979,0.,1.40243487042194));
#48225=CARTESIAN_POINT('Origin',(1.925,0.,0.84));
#48226=CARTESIAN_POINT('Origin',(1.925,0.,0.84));
#48227=CARTESIAN_POINT('',(1.77372658035123,0.197335634156047,0.22));
#48228=CARTESIAN_POINT('Origin',(2.04454922222021,0.,0.277565129578061));
#48229=CARTESIAN_POINT('',(1.71127058658217,0.0327612331676529,0.22));
#48230=CARTESIAN_POINT('Origin',(2.05937055187959,5.55111512312578E-17,
0.22));
#48231=CARTESIAN_POINT('Ctrl Pts',(1.51368509711198,0.0320423981330421,
1.34041816052587));
#48232=CARTESIAN_POINT('Ctrl Pts',(1.57907985889494,0.032336657496431,0.969593785059623));
#48233=CARTESIAN_POINT('Ctrl Pts',(1.64592664765089,0.0325785727668236,
0.590535829016318));
#48234=CARTESIAN_POINT('Ctrl Pts',(1.71127058658217,0.0327612331676708,
0.22));
#48235=CARTESIAN_POINT('Origin',(2.21659783251117,-0.858714575118933,0.3482551044561));
#48236=CARTESIAN_POINT('',(1.58266492545325,-0.824753943968933,0.22));
#48237=CARTESIAN_POINT('Origin',(1.90648537137062,-0.738576367636477,0.277565129578061));
#48238=CARTESIAN_POINT('',(1.76562782918999,-0.352472248043786,0.22));
#48239=CARTESIAN_POINT('Origin',(1.79500904160339,-0.69539020741027,0.84));
#48240=CARTESIAN_POINT('',(1.58387757652854,-0.648731178123907,0.22));
#48241=CARTESIAN_POINT('Ctrl Pts',(1.58387757652854,-0.648731178123902,
0.22));
#48242=CARTESIAN_POINT('Ctrl Pts',(1.52294492060034,-0.624929636779598,
0.590945123594562));
#48243=CARTESIAN_POINT('Ctrl Pts',(1.46074237258046,-0.600572896916442,
0.969742400014606));
#48244=CARTESIAN_POINT('Ctrl Pts',(1.39989426782994,-0.576684772985972,
1.34041816052587));
#48245=CARTESIAN_POINT('Origin',(1.92030584968083,-0.743930449457738,0.22));
#48246=CARTESIAN_POINT('Origin',(0.,0.,0.79));
#48247=CARTESIAN_POINT('',(-1.5105713967741,-1.84991642594294E-16,1.36));
#48248=CARTESIAN_POINT('Origin',(0.,0.,1.36));
#48249=CARTESIAN_POINT('',(-1.71158415478175,-2.09608605662479E-16,0.22));
#48250=CARTESIAN_POINT('',(-1.61107777577792,-1.97300124128387E-16,0.79));
#48251=CARTESIAN_POINT('',(-1.6881528136882,-0.282241734221848,0.22));
#48252=CARTESIAN_POINT('Origin',(0.,0.,0.22));
#48253=CARTESIAN_POINT('Ctrl Pts',(-1.6881528136882,-0.282241734221859,
0.22));
#48254=CARTESIAN_POINT('Ctrl Pts',(-1.62386387917194,-0.27040994350248,
0.590674417990065));
#48255=CARTESIAN_POINT('Ctrl Pts',(-1.55813030890113,-0.258368267043411,
0.969620067809347));
#48256=CARTESIAN_POINT('Ctrl Pts',(-1.49379950706012,-0.246642091306311,
1.34041816052587));
#48257=CARTESIAN_POINT('',(-1.47219814341721,-0.873013714336066,0.22));
#48258=CARTESIAN_POINT('Origin',(0.,0.,0.22));
#48259=CARTESIAN_POINT('Ctrl Pts',(-1.47219814341721,-0.873013714336065,
0.22));
#48260=CARTESIAN_POINT('Ctrl Pts',(-1.41643192586061,-0.838700012225428,
0.591291663208605));
#48261=CARTESIAN_POINT('Ctrl Pts',(-1.35953373199102,-0.803754548254296,
0.96992686245492));
#48262=CARTESIAN_POINT('Ctrl Pts',(-1.3038291566161,-0.769609523625295,
1.34041816052587));
#48263=CARTESIAN_POINT('',(-1.0574149561462,-1.3458803547932,0.22));
#48264=CARTESIAN_POINT('Origin',(0.,0.,0.22));
#48265=CARTESIAN_POINT('Ctrl Pts',(-1.05741495614621,-1.3458803547932,0.22));
#48266=CARTESIAN_POINT('Ctrl Pts',(-1.01779089885589,-1.29371349124397,
0.591471164251991));
#48267=CARTESIAN_POINT('Ctrl Pts',(-0.977366926097244,-1.24058473728836,
0.97002874200439));
#48268=CARTESIAN_POINT('Ctrl Pts',(-0.937769453804316,-1.18863692522509,
1.34041816052587));
#48269=CARTESIAN_POINT('',(-0.499822019709113,-1.63697839555501,0.22));
#48270=CARTESIAN_POINT('Origin',(0.,0.,0.22));
#48271=CARTESIAN_POINT('Ctrl Pts',(-0.499822019709112,-1.63697839555501,
0.22));
#48272=CARTESIAN_POINT('Ctrl Pts',(-0.481751415170154,-1.57413474259924,
0.590796411387241));
#48273=CARTESIAN_POINT('Ctrl Pts',(-0.463234151929265,-1.50993705749001,
0.969671099083018));
#48274=CARTESIAN_POINT('Ctrl Pts',(-0.445058789896327,-1.44713232360867,
1.34041816052587));
#48275=CARTESIAN_POINT('',(0.125274650099118,-1.70699343318669,0.22));
#48276=CARTESIAN_POINT('Origin',(0.,0.,0.22));
#48277=CARTESIAN_POINT('Ctrl Pts',(0.125274650099119,-1.70699343318669,
0.22));
#48278=CARTESIAN_POINT('Ctrl Pts',(0.119426587169905,-1.64190285944202,
0.59058437497945));
#48279=CARTESIAN_POINT('Ctrl Pts',(0.113500444422932,-1.57532801615826,
0.969590465098185));
#48280=CARTESIAN_POINT('Ctrl Pts',(0.107759529743048,-1.51018448285187,
1.34041816052587));
#48281=CARTESIAN_POINT('',(0.733452284240667,-1.54646954888937,0.22));
#48282=CARTESIAN_POINT('Origin',(0.,0.,0.22));
#48283=CARTESIAN_POINT('Ctrl Pts',(0.733452284240667,-1.54646954888937,
0.22));
#48284=CARTESIAN_POINT('Ctrl Pts',(0.704444345412884,-1.48780332282645,
0.591113453768949));
#48285=CARTESIAN_POINT('Ctrl Pts',(0.674891498357873,-1.42791069482832,
0.969829650214334));
#48286=CARTESIAN_POINT('Ctrl Pts',(0.64602432777446,-1.36927785946482,1.34041816052587));
#48287=CARTESIAN_POINT('',(1.2425731231961,-1.17708638273095,0.22));
#48288=CARTESIAN_POINT('Origin',(0.,0.,0.22));
#48289=CARTESIAN_POINT('Ctrl Pts',(1.2425731231961,-1.17708638273095,0.22));
#48290=CARTESIAN_POINT('Ctrl Pts',(1.19426284194958,-1.13279783604494,0.591640398518164));
#48291=CARTESIAN_POINT('Ctrl Pts',(1.14509967203354,-1.08765249687192,0.97012818472025));
#48292=CARTESIAN_POINT('Ctrl Pts',(1.09703996059555,-1.04344267372651,1.34041816052587));
#48293=CARTESIAN_POINT('Origin',(0.,0.,0.22));
#48294=CARTESIAN_POINT('',(1.71127058658217,-0.0327612331676529,0.22));
#48295=CARTESIAN_POINT('Origin',(0.,0.,0.22));
#48296=CARTESIAN_POINT('Ctrl Pts',(1.71127058658217,-0.0327612331676703,
0.22));
#48297=CARTESIAN_POINT('Ctrl Pts',(1.64592664790065,-0.0325785727675214,
0.590535827600031));
#48298=CARTESIAN_POINT('Ctrl Pts',(1.57907985913672,-0.0323366574975186,
0.96959378368857));
#48299=CARTESIAN_POINT('Ctrl Pts',(1.51368509711198,-0.0320423981330418,
1.34041816052587));
#48300=CARTESIAN_POINT('',(1.60754702144021,0.587633297864109,0.22));
#48301=CARTESIAN_POINT('Origin',(0.,0.,0.22));
#48302=CARTESIAN_POINT('Ctrl Pts',(1.60754702144021,0.587633297864116,0.22));
#48303=CARTESIAN_POINT('Ctrl Pts',(1.54648225330539,0.564172785329145,0.590945107425194));
#48304=CARTESIAN_POINT('Ctrl Pts',(1.48410498508378,0.540267047261947,0.969742390059058));
#48305=CARTESIAN_POINT('Ctrl Pts',(1.42304436641037,0.516927480140813,1.34041816052587));
#48306=CARTESIAN_POINT('',(1.2867153233272,1.12866469583084,0.22));
#48307=CARTESIAN_POINT('Origin',(0.,0.,0.22));
#48308=CARTESIAN_POINT('Ctrl Pts',(1.2867153233272,1.12866469583084,0.22));
#48309=CARTESIAN_POINT('Ctrl Pts',(1.23815819444723,1.08464693024256,0.591640390332101));
#48310=CARTESIAN_POINT('Ctrl Pts',(1.18866923188292,1.03985896774671,0.970128179719278));
#48311=CARTESIAN_POINT('Ctrl Pts',(1.14021360866399,0.996083437827605,1.34041816052587));
#48312=CARTESIAN_POINT('',(0.792105590863113,1.51726367247863,0.22));
#48313=CARTESIAN_POINT('Origin',(0.,0.,0.22));
#48314=CARTESIAN_POINT('Ctrl Pts',(0.79210559086311,1.51726367247863,0.22));
#48315=CARTESIAN_POINT('Ctrl Pts',(0.762770120472978,1.458760537755,0.591113453768949));
#48316=CARTESIAN_POINT('Ctrl Pts',(0.732784340782351,1.39908348459447,0.969829650214334));
#48317=CARTESIAN_POINT('Ctrl Pts',(0.703390684925826,1.34071280774691,1.34041816052587));
#48318=CARTESIAN_POINT('',(0.190517609144359,1.70094778270994,0.22));
#48319=CARTESIAN_POINT('Origin',(0.,0.,0.22));
#48320=CARTESIAN_POINT('Ctrl Pts',(0.190517609144358,1.70094778270994,0.22));
#48321=CARTESIAN_POINT('Ctrl Pts',(0.184305736149047,1.63589092093253,0.590584374979451));
#48322=CARTESIAN_POINT('Ctrl Pts',(0.177897879702104,1.56936071499665,0.969590465098185));
#48323=CARTESIAN_POINT('Ctrl Pts',(0.171570951566093,1.50427148383386,1.34041816052587));
#48324=CARTESIAN_POINT('',(-0.436800831383854,1.65490946960924,0.22));
#48325=CARTESIAN_POINT('Origin',(0.,0.,0.22));
#48326=CARTESIAN_POINT('Ctrl Pts',(-0.436800831383856,1.65490946960923,
0.22));
#48327=CARTESIAN_POINT('Ctrl Pts',(-0.419081848867252,1.59196577156245,
0.59079641138724));
#48328=CARTESIAN_POINT('Ctrl Pts',(-0.401029817157702,1.52763571666994,
0.969671099083018));
#48329=CARTESIAN_POINT('Ctrl Pts',(-0.383420389510104,1.46466996057301,
1.34041816052587));
#48330=CARTESIAN_POINT('',(-1.00512689923672,1.38536646246786,0.22));
#48331=CARTESIAN_POINT('Origin',(0.,0.,0.22));
#48332=CARTESIAN_POINT('Ctrl Pts',(-1.00512689923672,1.38536646246787,0.22));
#48333=CARTESIAN_POINT('Ctrl Pts',(-0.965795110148029,1.33297888821793,
0.591471164251991));
#48334=CARTESIAN_POINT('Ctrl Pts',(-0.925757057459429,1.27955870095344,
0.970028742004391));
#48335=CARTESIAN_POINT('Ctrl Pts',(-0.886628682377236,1.22725664312035,
1.34041816052587));
#48336=CARTESIAN_POINT('',(-1.43770500974724,0.928722037989635,0.22));
#48337=CARTESIAN_POINT('Origin',(0.,0.,0.22));
#48338=CARTESIAN_POINT('Ctrl Pts',(-1.43770500974724,0.928722037989638,
0.22));
#48339=CARTESIAN_POINT('Ctrl Pts',(-1.38213150110575,0.894097100294643,
0.591291663208604));
#48340=CARTESIAN_POINT('Ctrl Pts',(-1.32548789717734,0.858740459450525,
0.96992686245492));
#48341=CARTESIAN_POINT('Ctrl Pts',(-1.27009285871019,0.824095515550461,
1.34041816052587));
#48342=CARTESIAN_POINT('',(-1.67611309209293,0.346648556054452,0.22));
#48343=CARTESIAN_POINT('Origin',(0.,0.,0.22));
#48344=CARTESIAN_POINT('Ctrl Pts',(-1.67611309209293,0.346648556054445,
0.22));
#48345=CARTESIAN_POINT('Ctrl Pts',(-1.61189131020508,0.334457530502342,
0.590674417990065));
#48346=CARTESIAN_POINT('Ctrl Pts',(-1.54624662612018,0.321940354946836,
0.969620067809347));
#48347=CARTESIAN_POINT('Ctrl Pts',(-1.48202395664686,0.309635722134596,
1.34041816052587));
#48348=CARTESIAN_POINT('Origin',(0.,0.,0.22));
#48349=CARTESIAN_POINT('Origin',(1.75671243867939,-1.60145498856633,0.3482551044561));
#48350=CARTESIAN_POINT('',(1.17785560252371,-1.34078466352944,0.22));
#48351=CARTESIAN_POINT('Origin',(1.5109401069173,-1.37740390423071,0.277565129578061));
#48352=CARTESIAN_POINT('',(1.69921453277503,-0.768881160572422,0.22));
#48353=CARTESIAN_POINT('Origin',(1.42259216564977,-1.29686411401962,0.84));
#48354=CARTESIAN_POINT('Origin',(1.52189320170064,-1.38738896945528,0.22));
#48355=CARTESIAN_POINT('Origin',(1.05957329572431,-2.12791003183941,0.3482551044561));
#48356=CARTESIAN_POINT('',(0.613970353750137,-1.67573498473601,0.22));
#48357=CARTESIAN_POINT('Origin',(0.911334008616638,-1.83020541110008,0.277565129578061));
#48358=CARTESIAN_POINT('',(1.47637898190569,-1.24630651326724,0.22));
#48359=CARTESIAN_POINT('Origin',(0.858046334869837,-1.72318933585849,0.84));
#48360=CARTESIAN_POINT('Origin',(0.917940443729429,-1.84347292134022,0.22));
#48361=CARTESIAN_POINT('Origin',(0.219332907883337,-2.36697903415605,0.3482551044561));
#48362=CARTESIAN_POINT('',(-0.0328349934245695,-1.78436801068587,0.22));
#48363=CARTESIAN_POINT('Origin',(0.188647202576228,-2.0358275356821,0.277565129578061));
#48364=CARTESIAN_POINT('',(1.01216517589981,-1.68753448467274,0.22));
#48365=CARTESIAN_POINT('Origin',(0.177616591966855,-1.91678828936794,0.84));
#48366=CARTESIAN_POINT('Origin',(0.190014742348963,-2.05058564016207,0.22));
#48367=CARTESIAN_POINT('Origin',(-0.650529604532875,-2.28637440202631,0.3482551044561));
#48368=CARTESIAN_POINT('',(-0.675205792792306,-1.65201224926814,0.22));
#48369=CARTESIAN_POINT('Origin',(-0.559517453502335,-1.96649987066044,0.277565129578061));
#48370=CARTESIAN_POINT('',(0.306297263555869,-1.93127394609614,0.22));
#48371=CARTESIAN_POINT('Origin',(-0.52680125588876,-1.85151436310768,0.84));
#48372=CARTESIAN_POINT('Origin',(-0.563573502893763,-1.98075540559274,0.22));
#48373=CARTESIAN_POINT('Origin',(-1.43253448914795,-1.896982237665,0.3482551044561));
#48374=CARTESIAN_POINT('',(-1.22638630839899,-1.29654307947085,0.22));
#48375=CARTESIAN_POINT('Origin',(-1.23211617709217,-1.63158550135414,0.277565129578061));
#48376=CARTESIAN_POINT('',(-0.523913724701359,-1.82702575023449,0.22));
#48377=CARTESIAN_POINT('Origin',(-1.16007167503007,-1.53618316251446,0.84));
#48378=CARTESIAN_POINT('Origin',(-1.2410480237021,-1.64341317775352,0.22));
#48379=CARTESIAN_POINT('Origin',(-2.02106765305595,-1.25139211056558,0.3482551044561));
#48380=CARTESIAN_POINT('',(-1.61193655741525,-0.765968582397815,0.22));
#48381=CARTESIAN_POINT('Origin',(-1.73831078357428,-1.0763164691626,0.277565129578061));
#48382=CARTESIAN_POINT('',(-1.27088637074967,-1.31678354640376,0.22));
#48383=CARTESIAN_POINT('Origin',(-1.63666798627951,-1.01338191353891,0.84));
#48384=CARTESIAN_POINT('Origin',(-1.75091213202498,-1.0841188937919,0.22));
#48385=CARTESIAN_POINT('Origin',(-2.33664443129628,-0.43679454473122,0.3482551044561));
#48386=CARTESIAN_POINT('',(-1.77978584230378,-0.131945783893515,0.22));
#48387=CARTESIAN_POINT('Origin',(-2.00973688642211,-0.375684933735207,0.277565129578061));
#48388=CARTESIAN_POINT('',(-1.71463064913977,-0.480495281851195,0.22));
#48389=CARTESIAN_POINT('Origin',(-1.89222321689151,-0.353717821796897,0.84));
#48390=CARTESIAN_POINT('Origin',(-2.02430585477882,-0.378408345913518,0.22));
#48391=CARTESIAN_POINT('Origin',(-2.33664443129628,0.43679454473122,0.3482551044561));
#48392=CARTESIAN_POINT('',(-1.70726518705538,0.519897023862432,0.22));
#48393=CARTESIAN_POINT('Origin',(-2.00973688642211,0.375684933735208,0.277565129578061));
#48394=CARTESIAN_POINT('',(-1.71463064913977,0.480495281851196,0.22));
#48395=CARTESIAN_POINT('Origin',(-1.89222321689151,0.353717821796898,0.84));
#48396=CARTESIAN_POINT('Origin',(-2.02430585477882,0.378408345913518,0.22));
#48397=CARTESIAN_POINT('Origin',(-2.02106765305595,1.25139211056558,0.3482551044561));
#48398=CARTESIAN_POINT('',(-1.40416890801217,1.1015248576969,0.22));
#48399=CARTESIAN_POINT('Origin',(-1.73831078357428,1.0763164691626,0.277565129578061));
#48400=CARTESIAN_POINT('',(-1.27088637074967,1.31678354640376,0.22));
#48401=CARTESIAN_POINT('Origin',(-1.63666798627951,1.01338191353891,0.84));
#48402=CARTESIAN_POINT('Origin',(-1.75091213202497,1.0841188937919,0.22));
#48403=CARTESIAN_POINT('Origin',(-1.43253448914794,1.896982237665,0.3482551044561));
#48404=CARTESIAN_POINT('',(-0.911431837173392,1.53438565573945,0.22));
#48405=CARTESIAN_POINT('Origin',(-1.23211617709217,1.63158550135414,0.277565129578061));
#48406=CARTESIAN_POINT('',(-0.523913724701358,1.82702575023449,0.22));
#48407=CARTESIAN_POINT('Origin',(-1.16007167503007,1.53618316251446,0.84));
#48408=CARTESIAN_POINT('Origin',(-1.2410480237021,1.64341317775352,0.22));
#48409=CARTESIAN_POINT('Origin',(-0.650529604532875,2.28637440202631,0.3482551044561));
#48410=CARTESIAN_POINT('',(-0.295600846306193,1.76001916864997,0.22));
#48411=CARTESIAN_POINT('Origin',(-0.559517453502335,1.96649987066044,0.277565129578062));
#48412=CARTESIAN_POINT('',(0.30629726355587,1.93127394609614,0.22));
#48413=CARTESIAN_POINT('Origin',(-0.52680125588876,1.85151436310768,0.84));
#48414=CARTESIAN_POINT('Origin',(-0.563573502893763,1.98075540559275,0.22));
#48415=CARTESIAN_POINT('Origin',(0.219332907883338,2.36697903415605,0.3482551044561));
#48416=CARTESIAN_POINT('',(0.360152676835491,1.74795234023142,0.22));
#48417=CARTESIAN_POINT('Origin',(0.188647202576229,2.0358275356821,0.277565129578061));
#48418=CARTESIAN_POINT('',(1.01216517589981,1.68753448467274,0.22));
#48419=CARTESIAN_POINT('Origin',(0.177616591966856,1.91678828936794,0.84));
#48420=CARTESIAN_POINT('Origin',(0.190014742348964,2.05058564016207,0.22));
#48421=CARTESIAN_POINT('Origin',(1.05957329572431,2.12791003183941,0.3482551044561));
#48422=CARTESIAN_POINT('',(0.967265585295667,1.49981486252633,0.22));
#48423=CARTESIAN_POINT('Origin',(0.911334008616637,1.83020541110008,0.277565129578061));
#48424=CARTESIAN_POINT('',(1.47637898190569,1.24630651326724,0.22));
#48425=CARTESIAN_POINT('Origin',(0.858046334869836,1.7231893358585,0.84));
#48426=CARTESIAN_POINT('Origin',(0.917940443729428,1.84347292134022,0.22));
#48427=CARTESIAN_POINT('Origin',(1.75671243867939,1.60145498856633,0.3482551044561));
#48428=CARTESIAN_POINT('',(1.44374391665803,1.04911907687602,0.22));
#48429=CARTESIAN_POINT('Origin',(1.5109401069173,1.37740390423071,0.277565129578062));
#48430=CARTESIAN_POINT('',(1.69921453277503,0.768881160572423,0.22));
#48431=CARTESIAN_POINT('Origin',(1.42259216564977,1.29686411401962,0.84));
#48432=CARTESIAN_POINT('Origin',(1.52189320170064,1.38738896945528,0.22));
#48433=CARTESIAN_POINT('Origin',(2.21659783251117,0.858714575118932,0.3482551044561));
#48434=CARTESIAN_POINT('',(1.72523663201451,0.45673394652411,0.22));
#48435=CARTESIAN_POINT('Origin',(1.90648537137062,0.738576367636477,0.277565129578061));
#48436=CARTESIAN_POINT('',(1.76562782918999,0.352472248043786,0.22));
#48437=CARTESIAN_POINT('Origin',(1.79500904160339,0.695390207410269,0.84));
#48438=CARTESIAN_POINT('Origin',(1.92030584968083,0.743930449457738,0.22));
#48439=CARTESIAN_POINT('Origin',(1.925,0.,0.84));
#48440=CARTESIAN_POINT('',(1.77372658035123,-0.197335634156047,0.22));
#48441=CARTESIAN_POINT('Origin',(2.05937055187959,5.55111512312578E-17,
0.22));
#48442=CARTESIAN_POINT('Origin',(2.04454922222021,0.,0.277565129578061));
#48443=CARTESIAN_POINT('Origin',(2.37711940646971,0.,0.3482551044561));
#48444=CARTESIAN_POINT('',(1.77372658035123,0.,0.22));
#48445=CARTESIAN_POINT('Origin',(0.,0.,0.03));
#48446=CARTESIAN_POINT('',(-1.25,-1.53080849893419E-16,0.06));
#48447=CARTESIAN_POINT('Origin',(0.,0.,0.0599999999999999));
#48448=CARTESIAN_POINT('',(-1.31,-1.60428730688303E-16,2.08166817117217E-17));
#48449=CARTESIAN_POINT('',(-1.28,-1.56754790290861E-16,0.03));
#48450=CARTESIAN_POINT('Origin',(0.,0.,0.));
#48451=CARTESIAN_POINT('Origin',(1.84,0.,0.));
#48452=CARTESIAN_POINT('',(-1.84,-2.25335011043113E-16,1.73472347597681E-17));
#48453=CARTESIAN_POINT('Origin',(0.,0.,0.));
#48454=CARTESIAN_POINT('Origin',(0.,0.,0.03));
#48455=CARTESIAN_POINT('',(-1.9,-2.32682891837997E-16,0.06));
#48456=CARTESIAN_POINT('Origin',(0.,0.,0.0599999999999999));
#48457=CARTESIAN_POINT('',(-1.87,-2.29008951440555E-16,0.03));
#48458=CARTESIAN_POINT('Origin',(0.,0.,0.14));
#48459=CARTESIAN_POINT('',(-1.9,-2.32682891837997E-16,0.22));
#48460=CARTESIAN_POINT('Origin',(0.,0.,0.22));
#48461=CARTESIAN_POINT('',(-1.9,-2.32682891837997E-16,0.14));
#48462=CARTESIAN_POINT('Origin',(1.71158415478175,0.,0.22));
#48463=CARTESIAN_POINT('Origin',(1.6,0.,1.36));
#48464=CARTESIAN_POINT('',(-1.6,-1.95943487863577E-16,1.36));
#48465=CARTESIAN_POINT('Origin',(0.,0.,1.36));
#48466=CARTESIAN_POINT('Origin',(0.,0.,1.43));
#48467=CARTESIAN_POINT('',(-1.6,-1.95943487863577E-16,1.5));
#48468=CARTESIAN_POINT('Origin',(0.,0.,1.5));
#48469=CARTESIAN_POINT('',(-1.6,-1.95943487863577E-16,1.43));
#48470=CARTESIAN_POINT('Origin',(1.31,0.,1.5));
#48471=CARTESIAN_POINT('',(-1.31,-1.60428730688303E-16,1.5));
#48472=CARTESIAN_POINT('Origin',(0.,0.,1.5));
#48473=CARTESIAN_POINT('Origin',(0.,0.,1.47));
#48474=CARTESIAN_POINT('',(-1.25,-1.53080849893419E-16,1.44));
#48475=CARTESIAN_POINT('',(-1.28,-1.56754790290861E-16,1.47));
#48476=CARTESIAN_POINT('Origin',(0.,0.,1.44));
#48477=CARTESIAN_POINT('Origin',(0.,0.,0.75));
#48478=CARTESIAN_POINT('',(-1.25,-1.53080849893419E-16,0.75));
#59177=UNCERTAINTY_MEASURE_WITH_UNIT(LENGTH_MEASURE(0.001),#59205,
'DISTANCE_ACCURACY_VALUE',
'Maximum model space distance between geometric entities at asserted c
onnectivities');
#59182=UNCERTAINTY_MEASURE_WITH_UNIT(LENGTH_MEASURE(0.001),#59205,
'DISTANCE_ACCURACY_VALUE',
'Maximum model space distance between geometric entities at asserted c
onnectivities');
#59199=(
GEOMETRIC_REPRESENTATION_CONTEXT(3)
GLOBAL_UNCERTAINTY_ASSIGNED_CONTEXT((#59177))
GLOBAL_UNIT_ASSIGNED_CONTEXT((#59205,#59207,#59208))
REPRESENTATION_CONTEXT('','3D')
);
#59204=(
GEOMETRIC_REPRESENTATION_CONTEXT(3)
GLOBAL_UNCERTAINTY_ASSIGNED_CONTEXT((#59182))
GLOBAL_UNIT_ASSIGNED_CONTEXT((#59205,#59207,#59208))
REPRESENTATION_CONTEXT('','3D')
);
#59205=(
LENGTH_UNIT()
NAMED_UNIT(*)
SI_UNIT(.CENTI.,.METRE.)
);
#59207=(
NAMED_UNIT(*)
PLANE_ANGLE_UNIT()
SI_UNIT($,.RADIAN.)
);
#59208=(
NAMED_UNIT(*)
SI_UNIT($,.STERADIAN.)
SOLID_ANGLE_UNIT()
);
#59225=SHAPE_DEFINITION_REPRESENTATION(#59246,#59312);
#59246=PRODUCT_DEFINITION_SHAPE('',$,#59334);
#59312=SHAPE_REPRESENTATION('',(#24231),#59199);
#59317=PRODUCT_DEFINITION_CONTEXT('part definition',#59382,'design');
#59334=PRODUCT_DEFINITION('2026-10-23-00-47-28-876',
'12_Taper_Roller_Bearing_30205_Cone_Assembly',#59355,#59317);
#59355=PRODUCT_DEFINITION_FORMATION('',$,#59400);
#59382=APPLICATION_CONTEXT(
'Core Data for Automotive Mechanical Design Process');
#59383=PRODUCT_CONTEXT('part definition',#59382,'mechanical');
#59400=PRODUCT('2026-10-23-00-47-28-876',
'12_Taper_Roller_Bearing_30205_Cone_Assembly',$,(#59383));
#59580=COLOUR_RGB('Grey',0.48,0.52,0.57);
#59581=FILL_AREA_STYLE_COLOUR('',#59580);
#59582=FILL_AREA_STYLE('',(#59581));
#59583=SURFACE_STYLE_FILL_AREA(#59582);
#59584=SURFACE_SIDE_STYLE('',(#59583));
#59585=SURFACE_STYLE_USAGE(.BOTH.,#59584);
#59586=PRESENTATION_STYLE_ASSIGNMENT((#59585));
ENDSEC;
END-ISO-10303-21;
